ISO-10303-21;
HEADER;
FILE_DESCRIPTION((''),'2;1');
FILE_NAME('Flat_Washer_Large.step','2026-10-09T10:33:02-07:00',(''),(''),'','','');
FILE_SCHEMA (('AUTOMOTIVE_DESIGN { 1 0 10303 214 3 1 1 }'));
ENDSEC;
DATA;
#10=MECHANICAL_DESIGN_GEOMETRIC_PRESENTATION_REPRESENTATION('',(#845),#86330);
#456=TOROIDAL_SURFACE('',#36171,0.730250002805488,0.0952500026781452) ;
#457=TOROIDAL_SURFACE('',#36179,0.730250002805489,0.0952500026781457) ;
#458=TOROIDAL_SURFACE('',#36187,0.730250002805489,0.0952500026781457) ;
#459=TOROIDAL_SURFACE('',#36205,0.571500002095673,0.0634999979994503) ;
#460=TOROIDAL_SURFACE('',#36208,0.571500002095676,0.0634999979994492) ;
#461=TOROIDAL_SURFACE('',#36220,0.571500002095676,0.0634999979994491) ;
#462=TOROIDAL_SURFACE('',#36237,0.571500002095674,0.0634999979994503) ;
#463=TOROIDAL_SURFACE('',#36240,0.730250002805489,0.0952500026781457) ;
#464=TOROIDAL_SURFACE('',#36260,0.445134999999998,0.189865000000001) ;
#465=TOROIDAL_SURFACE('',#36274,0.445134999999997,0.189865000000001) ;
#466=TOROIDAL_SURFACE('',#36288,0.445134999999999,0.189865) ;
#467=TOROIDAL_SURFACE('',#36302,0.445134999999993,0.189865000000003) ;
#748=(
BOUNDED_SURFACE()
B_SPLINE_SURFACE(2,2,((#80804,#80805,#80806,#80807,#80808,#80809,#80810,
#80811,#80812),(#80813,#80814,#80815,#80816,#80817,#80818,#80819,#80820,
#80821),(#80822,#80823,#80824,#80825,#80826,#80827,#80828,#80829,#80830)),
 .UNSPECIFIED.,.F.,.T.,.F.)
B_SPLINE_SURFACE_WITH_KNOTS((3,3),(3,2,2,2,3),(0.,1.3),(0.,13.3286488144751,
26.6572976289502,39.9859464434253,53.3145952579004),.UNSPECIFIED.)
GEOMETRIC_REPRESENTATION_ITEM()
RATIONAL_B_SPLINE_SURFACE(((1.,0.707106781186548,1.,0.707106781186548,1.,
0.707106781186548,1.,0.707106781186548,1.),(1.,0.707106781186548,1.,0.707106781186548,
1.,0.707106781186548,1.,0.707106781186548,1.),(1.,0.707106781186548,1.,
0.707106781186548,1.,0.707106781186548,1.,0.707106781186548,1.)))
REPRESENTATION_ITEM('')
SURFACE()
) ;
#749=(
BOUNDED_SURFACE()
B_SPLINE_SURFACE(2,2,((#80847,#80848,#80849,#80850,#80851,#80852,#80853,
#80854,#80855),(#80856,#80857,#80858,#80859,#80860,#80861,#80862,#80863,
#80864),(#80865,#80866,#80867,#80868,#80869,#80870,#80871,#80872,#80873)),
 .UNSPECIFIED.,.F.,.T.,.F.)
B_SPLINE_SURFACE_WITH_KNOTS((3,3),(3,2,2,2,3),(0.,1.3),(0.,13.3286488144751,
26.6572976289502,39.9859464434253,53.3145952579004),.UNSPECIFIED.)
GEOMETRIC_REPRESENTATION_ITEM()
RATIONAL_B_SPLINE_SURFACE(((1.,0.707106781186548,1.,0.707106781186548,1.,
0.707106781186548,1.,0.707106781186548,1.),(1.,0.707106781186548,1.,0.707106781186548,
1.,0.707106781186548,1.,0.707106781186548,1.),(1.,0.707106781186548,1.,
0.707106781186548,1.,0.707106781186548,1.,0.707106781186548,1.)))
REPRESENTATION_ITEM('')
SURFACE()
) ;
#750=(
BOUNDED_SURFACE()
B_SPLINE_SURFACE(2,2,((#80892,#80893,#80894,#80895,#80896,#80897,#80898,
#80899,#80900),(#80901,#80902,#80903,#80904,#80905,#80906,#80907,#80908,
#80909),(#80910,#80911,#80912,#80913,#80914,#80915,#80916,#80917,#80918)),
 .UNSPECIFIED.,.F.,.T.,.F.)
B_SPLINE_SURFACE_WITH_KNOTS((3,3),(3,2,2,2,3),(0.,1.3),(0.,13.3286488144751,
26.6572976289502,39.9859464434253,53.3145952579004),.UNSPECIFIED.)
GEOMETRIC_REPRESENTATION_ITEM()
RATIONAL_B_SPLINE_SURFACE(((1.,0.707106781186548,1.,0.707106781186548,1.,
0.707106781186548,1.,0.707106781186548,1.),(1.,0.707106781186548,1.,0.707106781186548,
1.,0.707106781186548,1.,0.707106781186548,1.),(1.,0.707106781186548,1.,
0.707106781186548,1.,0.707106781186548,1.,0.707106781186548,1.)))
REPRESENTATION_ITEM('')
SURFACE()
) ;
#751=(
BOUNDED_SURFACE()
B_SPLINE_SURFACE(2,2,((#80929,#80930,#80931,#80932,#80933,#80934,#80935,
#80936,#80937),(#80938,#80939,#80940,#80941,#80942,#80943,#80944,#80945,
#80946),(#80947,#80948,#80949,#80950,#80951,#80952,#80953,#80954,#80955)),
 .UNSPECIFIED.,.F.,.T.,.F.)
B_SPLINE_SURFACE_WITH_KNOTS((3,3),(3,2,2,2,3),(0.,1.3),(0.,13.3286488144751,
26.6572976289502,39.9859464434253,53.3145952579004),.UNSPECIFIED.)
GEOMETRIC_REPRESENTATION_ITEM()
RATIONAL_B_SPLINE_SURFACE(((1.,0.707106781186548,1.,0.707106781186548,1.,
0.707106781186548,1.,0.707106781186548,1.),(1.,0.707106781186548,1.,0.707106781186548,
1.,0.707106781186548,1.,0.707106781186548,1.),(1.,0.707106781186548,1.,
0.707106781186548,1.,0.707106781186548,1.,0.707106781186548,1.)))
REPRESENTATION_ITEM('')
SURFACE()
) ;
#752=(
BOUNDED_SURFACE()
B_SPLINE_SURFACE(2,2,((#80974,#80975,#80976,#80977,#80978,#80979,#80980,
#80981,#80982),(#80983,#80984,#80985,#80986,#80987,#80988,#80989,#80990,
#80991),(#80992,#80993,#80994,#80995,#80996,#80997,#80998,#80999,#81000)),
 .UNSPECIFIED.,.F.,.T.,.F.)
B_SPLINE_SURFACE_WITH_KNOTS((3,3),(3,2,2,2,3),(0.,1.3),(0.,13.3286488144751,
26.6572976289502,39.9859464434253,53.3145952579004),.UNSPECIFIED.)
GEOMETRIC_REPRESENTATION_ITEM()
RATIONAL_B_SPLINE_SURFACE(((1.,0.707106781186548,1.,0.707106781186548,1.,
0.707106781186548,1.,0.707106781186548,1.),(1.,0.707106781186548,1.,0.707106781186548,
1.,0.707106781186548,1.,0.707106781186548,1.),(1.,0.707106781186548,1.,
0.707106781186548,1.,0.707106781186548,1.,0.707106781186548,1.)))
REPRESENTATION_ITEM('')
SURFACE()
) ;
#753=(
BOUNDED_SURFACE()
B_SPLINE_SURFACE(2,2,((#81429,#81430,#81431),(#81432,#81433,#81434),(#81435,
#81436,#81437),(#81438,#81439,#81440),(#81441,#81442,#81443),(#81444,#81445,
#81446),(#81447,#81448,#81449),(#81450,#81451,#81452),(#81453,#81454,#81455)),
 .UNSPECIFIED.,.T.,.F.,.F.)
B_SPLINE_SURFACE_WITH_KNOTS((3,2,2,2,3),(3,3),(0.,13.3286488144751,26.6572976289502,
39.9859464434253,53.3145952579004),(0.,1.3),.UNSPECIFIED.)
GEOMETRIC_REPRESENTATION_ITEM()
RATIONAL_B_SPLINE_SURFACE(((1.,1.,1.),(0.707106781186548,0.707106781186548,
0.707106781186548),(1.,1.,1.),(0.707106781186548,0.707106781186548,0.707106781186548),
(1.,1.,1.),(0.707106781186548,0.707106781186548,0.707106781186548),(1.,
1.,1.),(0.707106781186548,0.707106781186548,0.707106781186548),(1.,1.,1.)))
REPRESENTATION_ITEM('')
SURFACE()
) ;
#754=(
BOUNDED_SURFACE()
B_SPLINE_SURFACE(2,2,((#81475,#81476,#81477),(#81478,#81479,#81480),(#81481,
#81482,#81483),(#81484,#81485,#81486),(#81487,#81488,#81489),(#81490,#81491,
#81492),(#81493,#81494,#81495),(#81496,#81497,#81498),(#81499,#81500,#81501)),
 .UNSPECIFIED.,.T.,.F.,.F.)
B_SPLINE_SURFACE_WITH_KNOTS((3,2,2,2,3),(3,3),(0.,13.3286488144751,26.6572976289502,
39.9859464434253,53.3145952579004),(0.,1.3),.UNSPECIFIED.)
GEOMETRIC_REPRESENTATION_ITEM()
RATIONAL_B_SPLINE_SURFACE(((1.,1.,1.),(0.707106781186548,0.707106781186548,
0.707106781186548),(1.,1.,1.),(0.707106781186548,0.707106781186548,0.707106781186548),
(1.,1.,1.),(0.707106781186548,0.707106781186548,0.707106781186548),(1.,
1.,1.),(0.707106781186548,0.707106781186548,0.707106781186548),(1.,1.,1.)))
REPRESENTATION_ITEM('')
SURFACE()
) ;
#755=(
BOUNDED_SURFACE()
B_SPLINE_SURFACE(2,2,((#81521,#81522,#81523),(#81524,#81525,#81526),(#81527,
#81528,#81529),(#81530,#81531,#81532),(#81533,#81534,#81535),(#81536,#81537,
#81538),(#81539,#81540,#81541),(#81542,#81543,#81544),(#81545,#81546,#81547)),
 .UNSPECIFIED.,.T.,.F.,.F.)
B_SPLINE_SURFACE_WITH_KNOTS((3,2,2,2,3),(3,3),(0.,13.3286488144751,26.6572976289502,
39.9859464434253,53.3145952579004),(0.,1.3),.UNSPECIFIED.)
GEOMETRIC_REPRESENTATION_ITEM()
RATIONAL_B_SPLINE_SURFACE(((1.,1.,1.),(0.707106781186548,0.707106781186548,
0.707106781186548),(1.,1.,1.),(0.707106781186548,0.707106781186548,0.707106781186548),
(1.,1.,1.),(0.707106781186548,0.707106781186548,0.707106781186548),(1.,
1.,1.),(0.707106781186548,0.707106781186548,0.707106781186548),(1.,1.,1.)))
REPRESENTATION_ITEM('')
SURFACE()
) ;
#756=(
BOUNDED_SURFACE()
B_SPLINE_SURFACE(2,2,((#81561,#81562,#81563),(#81564,#81565,#81566),(#81567,
#81568,#81569),(#81570,#81571,#81572),(#81573,#81574,#81575),(#81576,#81577,
#81578),(#81579,#81580,#81581),(#81582,#81583,#81584),(#81585,#81586,#81587)),
 .UNSPECIFIED.,.T.,.F.,.F.)
B_SPLINE_SURFACE_WITH_KNOTS((3,2,2,2,3),(3,3),(0.,13.3286488144751,26.6572976289502,
39.9859464434253,53.3145952579004),(0.,1.3),.UNSPECIFIED.)
GEOMETRIC_REPRESENTATION_ITEM()
RATIONAL_B_SPLINE_SURFACE(((1.,1.,1.),(0.707106781186548,0.707106781186548,
0.707106781186548),(1.,1.,1.),(0.707106781186548,0.707106781186548,0.707106781186548),
(1.,1.,1.),(0.707106781186548,0.707106781186548,0.707106781186548),(1.,
1.,1.),(0.707106781186548,0.707106781186548,0.707106781186548),(1.,1.,1.)))
REPRESENTATION_ITEM('')
SURFACE()
) ;
#757=(
BOUNDED_SURFACE()
B_SPLINE_SURFACE(2,2,((#81600,#81601,#81602),(#81603,#81604,#81605),(#81606,
#81607,#81608),(#81609,#81610,#81611),(#81612,#81613,#81614),(#81615,#81616,
#81617),(#81618,#81619,#81620),(#81621,#81622,#81623),(#81624,#81625,#81626)),
 .UNSPECIFIED.,.T.,.F.,.F.)
B_SPLINE_SURFACE_WITH_KNOTS((3,2,2,2,3),(3,3),(0.,13.3286488144751,26.6572976289502,
39.9859464434253,53.3145952579004),(0.,1.3),.UNSPECIFIED.)
GEOMETRIC_REPRESENTATION_ITEM()
RATIONAL_B_SPLINE_SURFACE(((1.,1.,1.),(0.707106781186548,0.707106781186548,
0.707106781186548),(1.,1.,1.),(0.707106781186548,0.707106781186548,0.707106781186548),
(1.,1.,1.),(0.707106781186548,0.707106781186548,0.707106781186548),(1.,
1.,1.),(0.707106781186548,0.707106781186548,0.707106781186548),(1.,1.,1.)))
REPRESENTATION_ITEM('')
SURFACE()
) ;
#821=SHAPE_REPRESENTATION_RELATIONSHIP('SRR','None',#86467,#833) ;
#833=ADVANCED_BREP_SHAPE_REPRESENTATION('',(#857),#86321) ;
#845=STYLED_ITEM('',(#86582),#857) ;
#857=MANIFOLD_SOLID_BREP('Body1',#32644) ;
#1173=FACE_BOUND('',#6029,.T.) ;
#1174=FACE_BOUND('',#6103,.T.) ;
#1612=B_SPLINE_CURVE_WITH_KNOTS('',3,(#80833,#80834,#80835,#80836,#80837,
#80838),.UNSPECIFIED.,.F.,.F.,(4,2,4),(-0.0629976158763524,-0.0314993212424117,
-1.00009004573627E-6),.UNSPECIFIED.) ;
#1613=B_SPLINE_CURVE_WITH_KNOTS('',3,(#80842,#80843,#80844,#80845),
 .UNSPECIFIED.,.F.,.F.,(4,4),(0.65,1.3),.UNSPECIFIED.) ;
#1614=B_SPLINE_CURVE_WITH_KNOTS('',3,(#80876,#80877,#80878,#80879,#80880,
#80881),.UNSPECIFIED.,.F.,.F.,(4,2,4),(-0.0629976151793818,-0.0314998208710405,
-9.99993644668074E-7),.UNSPECIFIED.) ;
#1615=B_SPLINE_CURVE_WITH_KNOTS('',3,(#80885,#80886,#80887,#80888,#80889,
#80890),.UNSPECIFIED.,.F.,.F.,(4,2,4),(-0.0749709647986248,-0.0374848715520891,
0.),.UNSPECIFIED.) ;
#1616=B_SPLINE_CURVE_WITH_KNOTS('',3,(#80922,#80923,#80924,#80925,#80926,
#80927),.UNSPECIFIED.,.F.,.F.,(4,2,4),(-0.0749708491846415,-0.0374854095897592,
0.),.UNSPECIFIED.) ;
#1617=B_SPLINE_CURVE_WITH_KNOTS('',3,(#80958,#80959,#80960,#80961,#80962,
#80963),.UNSPECIFIED.,.F.,.F.,(4,2,4),(-0.0629976151789191,-0.0314993208821172,
-9.999936648616E-7),.UNSPECIFIED.) ;
#1618=B_SPLINE_CURVE_WITH_KNOTS('',3,(#80967,#80968,#80969,#80970,#80971,
#80972),.UNSPECIFIED.,.F.,.F.,(4,2,4),(-0.074970850289862,-0.0374860052740206,
0.),.UNSPECIFIED.) ;
#1619=B_SPLINE_CURVE_WITH_KNOTS('',3,(#81003,#81004,#81005,#81006,#81007,
#81008),.UNSPECIFIED.,.F.,.F.,(4,2,4),(-0.0629976791811074,-0.0314988521171933,
-9.99993650290977E-7),.UNSPECIFIED.) ;
#1620=B_SPLINE_CURVE_WITH_KNOTS('',3,(#81012,#81013,#81014,#81015,#81016,
#81017),.UNSPECIFIED.,.F.,.F.,(4,2,4),(-0.0749709647978269,-0.0374854665776717,
0.),.UNSPECIFIED.) ;
#1621=B_SPLINE_CURVE_WITH_KNOTS('',3,(#81459,#81460,#81461,#81462,#81463,
#81464),.UNSPECIFIED.,.F.,.F.,(4,2,4),(9.99986190228668E-7,0.0314993519488164,
0.0629976787086803),.UNSPECIFIED.) ;
#1622=B_SPLINE_CURVE_WITH_KNOTS('',3,(#81465,#81466,#81467,#81468,#81469,
#81470),.UNSPECIFIED.,.F.,.F.,(4,2,4),(0.,0.0374854669831317,0.0749709656293669),
 .UNSPECIFIED.) ;
#1623=B_SPLINE_CURVE_WITH_KNOTS('',3,(#81505,#81506,#81507,#81508,#81509,
#81510),.UNSPECIFIED.,.F.,.F.,(4,2,4),(9.99986130257806E-7,0.0314993519482237,
0.0629976787077657),.UNSPECIFIED.) ;
#1624=B_SPLINE_CURVE_WITH_KNOTS('',3,(#81511,#81512,#81513,#81514,#81515,
#81516),.UNSPECIFIED.,.F.,.F.,(4,2,4),(0.,0.0374854669835134,0.0749709656299367),
 .UNSPECIFIED.) ;
#1625=B_SPLINE_CURVE_WITH_KNOTS('',3,(#81551,#81552,#81553,#81554,#81555,
#81556),.UNSPECIFIED.,.F.,.F.,(4,2,4),(9.99897261200662E-7,0.0314993517939326,
0.0629976784770454),.UNSPECIFIED.) ;
#1626=B_SPLINE_CURVE_WITH_KNOTS('',3,(#81557,#81558,#81559,#81560),
 .UNSPECIFIED.,.F.,.F.,(4,4),(0.65,1.3),.UNSPECIFIED.) ;
#1627=B_SPLINE_CURVE_WITH_KNOTS('',3,(#81590,#81591,#81592,#81593,#81594,
#81595),.UNSPECIFIED.,.F.,.F.,(4,2,4),(0.,0.0374854671857389,0.0749709659305387),
 .UNSPECIFIED.) ;
#1628=B_SPLINE_CURVE_WITH_KNOTS('',3,(#81630,#81631,#81632,#81633,#81634,
#81635),.UNSPECIFIED.,.F.,.F.,(4,2,4),(9.99986221142887E-7,0.0314993519490406,
0.0629976787097528),.UNSPECIFIED.) ;
#1629=B_SPLINE_CURVE_WITH_KNOTS('',3,(#81636,#81637,#81638,#81639,#81640,
#81641),.UNSPECIFIED.,.F.,.F.,(4,2,4),(0.,0.0374854669835796,0.0749709656310599),
 .UNSPECIFIED.) ;
#2191=PLANE('',#36158) ;
#2192=PLANE('',#36163) ;
#2193=PLANE('',#36165) ;
#2194=PLANE('',#36167) ;
#2195=PLANE('',#36169) ;
#2196=PLANE('',#36195) ;
#2197=PLANE('',#36196) ;
#2198=PLANE('',#36206) ;
#2199=PLANE('',#36207) ;
#2200=PLANE('',#36216) ;
#2201=PLANE('',#36217) ;
#2202=PLANE('',#36227) ;
#2203=PLANE('',#36228) ;
#2204=PLANE('',#36247) ;
#2205=PLANE('',#36249) ;
#2206=PLANE('',#36250) ;
#2207=PLANE('',#36261) ;
#2208=PLANE('',#36263) ;
#2209=PLANE('',#36264) ;
#2210=PLANE('',#36275) ;
#2211=PLANE('',#36277) ;
#2212=PLANE('',#36278) ;
#2213=PLANE('',#36289) ;
#2214=PLANE('',#36291) ;
#2215=PLANE('',#36292) ;
#2216=PLANE('',#36303) ;
#2217=PLANE('',#36304) ;
#2218=PLANE('',#36305) ;
#2219=PLANE('',#36306) ;
#2220=PLANE('',#36307) ;
#2221=PLANE('',#36314) ;
#2222=PLANE('',#36315) ;
#2223=PLANE('',#36317) ;
#2224=PLANE('',#36318) ;
#2225=PLANE('',#36321) ;
#2226=PLANE('',#36322) ;
#2227=PLANE('',#36324) ;
#2228=PLANE('',#36325) ;
#3961=FACE_OUTER_BOUND('',#6022,.T.) ;
#3962=FACE_OUTER_BOUND('',#6023,.T.) ;
#3963=FACE_OUTER_BOUND('',#6024,.T.) ;
#3964=FACE_OUTER_BOUND('',#6025,.T.) ;
#3965=FACE_OUTER_BOUND('',#6026,.T.) ;
#3966=FACE_OUTER_BOUND('',#6027,.T.) ;
#3967=FACE_OUTER_BOUND('',#6028,.T.) ;
#3968=FACE_OUTER_BOUND('',#6030,.T.) ;
#3969=FACE_OUTER_BOUND('',#6031,.T.) ;
#3970=FACE_OUTER_BOUND('',#6032,.T.) ;
#3971=FACE_OUTER_BOUND('',#6033,.T.) ;
#3972=FACE_OUTER_BOUND('',#6034,.T.) ;
#3973=FACE_OUTER_BOUND('',#6035,.T.) ;
#3974=FACE_OUTER_BOUND('',#6036,.T.) ;
#3975=FACE_OUTER_BOUND('',#6037,.T.) ;
#3976=FACE_OUTER_BOUND('',#6038,.T.) ;
#3977=FACE_OUTER_BOUND('',#6039,.T.) ;
#3978=FACE_OUTER_BOUND('',#6040,.T.) ;
#3979=FACE_OUTER_BOUND('',#6041,.T.) ;
#3980=FACE_OUTER_BOUND('',#6042,.T.) ;
#3981=FACE_OUTER_BOUND('',#6043,.T.) ;
#3982=FACE_OUTER_BOUND('',#6044,.T.) ;
#3983=FACE_OUTER_BOUND('',#6045,.T.) ;
#3984=FACE_OUTER_BOUND('',#6046,.T.) ;
#3985=FACE_OUTER_BOUND('',#6047,.T.) ;
#3986=FACE_OUTER_BOUND('',#6048,.T.) ;
#3987=FACE_OUTER_BOUND('',#6049,.T.) ;
#3988=FACE_OUTER_BOUND('',#6050,.T.) ;
#3989=FACE_OUTER_BOUND('',#6051,.T.) ;
#3990=FACE_OUTER_BOUND('',#6052,.T.) ;
#3991=FACE_OUTER_BOUND('',#6053,.T.) ;
#3992=FACE_OUTER_BOUND('',#6054,.T.) ;
#3993=FACE_OUTER_BOUND('',#6055,.T.) ;
#3994=FACE_OUTER_BOUND('',#6056,.T.) ;
#3995=FACE_OUTER_BOUND('',#6057,.T.) ;
#3996=FACE_OUTER_BOUND('',#6058,.T.) ;
#3997=FACE_OUTER_BOUND('',#6059,.T.) ;
#3998=FACE_OUTER_BOUND('',#6060,.T.) ;
#3999=FACE_OUTER_BOUND('',#6061,.T.) ;
#4000=FACE_OUTER_BOUND('',#6062,.T.) ;
#4001=FACE_OUTER_BOUND('',#6063,.T.) ;
#4002=FACE_OUTER_BOUND('',#6064,.T.) ;
#4003=FACE_OUTER_BOUND('',#6065,.T.) ;
#4004=FACE_OUTER_BOUND('',#6066,.T.) ;
#4005=FACE_OUTER_BOUND('',#6067,.T.) ;
#4006=FACE_OUTER_BOUND('',#6068,.T.) ;
#4007=FACE_OUTER_BOUND('',#6069,.T.) ;
#4008=FACE_OUTER_BOUND('',#6070,.T.) ;
#4009=FACE_OUTER_BOUND('',#6071,.T.) ;
#4010=FACE_OUTER_BOUND('',#6072,.T.) ;
#4011=FACE_OUTER_BOUND('',#6073,.T.) ;
#4012=FACE_OUTER_BOUND('',#6074,.T.) ;
#4013=FACE_OUTER_BOUND('',#6075,.T.) ;
#4014=FACE_OUTER_BOUND('',#6076,.T.) ;
#4015=FACE_OUTER_BOUND('',#6077,.T.) ;
#4016=FACE_OUTER_BOUND('',#6078,.T.) ;
#4017=FACE_OUTER_BOUND('',#6079,.T.) ;
#4018=FACE_OUTER_BOUND('',#6080,.T.) ;
#4019=FACE_OUTER_BOUND('',#6081,.T.) ;
#4020=FACE_OUTER_BOUND('',#6082,.T.) ;
#4021=FACE_OUTER_BOUND('',#6083,.T.) ;
#4022=FACE_OUTER_BOUND('',#6084,.T.) ;
#4023=FACE_OUTER_BOUND('',#6085,.T.) ;
#4024=FACE_OUTER_BOUND('',#6086,.T.) ;
#4025=FACE_OUTER_BOUND('',#6087,.T.) ;
#4026=FACE_OUTER_BOUND('',#6088,.T.) ;
#4027=FACE_OUTER_BOUND('',#6089,.T.) ;
#4028=FACE_OUTER_BOUND('',#6090,.T.) ;
#4029=FACE_OUTER_BOUND('',#6091,.T.) ;
#4030=FACE_OUTER_BOUND('',#6092,.T.) ;
#4031=FACE_OUTER_BOUND('',#6093,.T.) ;
#4032=FACE_OUTER_BOUND('',#6094,.T.) ;
#4033=FACE_OUTER_BOUND('',#6095,.T.) ;
#4034=FACE_OUTER_BOUND('',#6096,.T.) ;
#4035=FACE_OUTER_BOUND('',#6097,.T.) ;
#4036=FACE_OUTER_BOUND('',#6098,.T.) ;
#4037=FACE_OUTER_BOUND('',#6099,.T.) ;
#4038=FACE_OUTER_BOUND('',#6100,.T.) ;
#4039=FACE_OUTER_BOUND('',#6101,.T.) ;
#4040=FACE_OUTER_BOUND('',#6102,.T.) ;
#4041=FACE_OUTER_BOUND('',#6104,.T.) ;
#4042=FACE_OUTER_BOUND('',#6105,.T.) ;
#4043=FACE_OUTER_BOUND('',#6106,.T.) ;
#4044=FACE_OUTER_BOUND('',#6107,.T.) ;
#4045=FACE_OUTER_BOUND('',#6108,.T.) ;
#4046=FACE_OUTER_BOUND('',#6109,.T.) ;
#4047=FACE_OUTER_BOUND('',#6110,.T.) ;
#4048=FACE_OUTER_BOUND('',#6111,.T.) ;
#4049=FACE_OUTER_BOUND('',#6112,.T.) ;
#4050=FACE_OUTER_BOUND('',#6113,.T.) ;
#4051=FACE_OUTER_BOUND('',#6114,.T.) ;
#4052=FACE_OUTER_BOUND('',#6115,.T.) ;
#4053=FACE_OUTER_BOUND('',#6116,.T.) ;
#4054=FACE_OUTER_BOUND('',#6117,.T.) ;
#4055=FACE_OUTER_BOUND('',#6118,.T.) ;
#4056=FACE_OUTER_BOUND('',#6119,.T.) ;
#4057=FACE_OUTER_BOUND('',#6120,.T.) ;
#6022=EDGE_LOOP('',(#28914,#28915,#28916,#28917)) ;
#6023=EDGE_LOOP('',(#28918,#28919,#28920,#28921)) ;
#6024=EDGE_LOOP('',(#28922,#28923,#28924,#28925)) ;
#6025=EDGE_LOOP('',(#28926,#28927,#28928,#28929)) ;
#6026=EDGE_LOOP('',(#28930,#28931,#28932,#28933)) ;
#6027=EDGE_LOOP('',(#28934,#28935,#28936,#28937)) ;
#6028=EDGE_LOOP('',(#28938,#28939,#28940,#28941,#28942,#28943,#28944,#28945,
#28946,#28947,#28948,#28949,#28950,#28951,#28952,#28953,#28954,#28955,#28956,
#28957,#28958,#28959,#28960,#28961,#28962)) ;
#6029=EDGE_LOOP('',(#28963)) ;
#6030=EDGE_LOOP('',(#28964,#28965,#28966,#28967)) ;
#6031=EDGE_LOOP('',(#28968,#28969,#28970,#28971)) ;
#6032=EDGE_LOOP('',(#28972,#28973,#28974,#28975)) ;
#6033=EDGE_LOOP('',(#28976,#28977,#28978,#28979)) ;
#6034=EDGE_LOOP('',(#28980,#28981,#28982,#28983)) ;
#6035=EDGE_LOOP('',(#28984,#28985,#28986,#28987)) ;
#6036=EDGE_LOOP('',(#28988,#28989,#28990,#28991)) ;
#6037=EDGE_LOOP('',(#28992,#28993,#28994,#28995)) ;
#6038=EDGE_LOOP('',(#28996,#28997,#28998,#28999)) ;
#6039=EDGE_LOOP('',(#29000,#29001,#29002,#29003)) ;
#6040=EDGE_LOOP('',(#29004,#29005,#29006,#29007)) ;
#6041=EDGE_LOOP('',(#29008,#29009,#29010,#29011)) ;
#6042=EDGE_LOOP('',(#29012,#29013,#29014,#29015)) ;
#6043=EDGE_LOOP('',(#29016,#29017,#29018,#29019)) ;
#6044=EDGE_LOOP('',(#29020,#29021,#29022,#29023)) ;
#6045=EDGE_LOOP('',(#29024,#29025,#29026,#29027)) ;
#6046=EDGE_LOOP('',(#29028,#29029,#29030,#29031)) ;
#6047=EDGE_LOOP('',(#29032,#29033,#29034,#29035)) ;
#6048=EDGE_LOOP('',(#29036,#29037,#29038,#29039)) ;
#6049=EDGE_LOOP('',(#29040,#29041,#29042,#29043)) ;
#6050=EDGE_LOOP('',(#29044,#29045,#29046,#29047)) ;
#6051=EDGE_LOOP('',(#29048,#29049,#29050,#29051)) ;
#6052=EDGE_LOOP('',(#29052,#29053,#29054,#29055)) ;
#6053=EDGE_LOOP('',(#29056,#29057,#29058,#29059)) ;
#6054=EDGE_LOOP('',(#29060,#29061,#29062,#29063)) ;
#6055=EDGE_LOOP('',(#29064,#29065,#29066,#29067)) ;
#6056=EDGE_LOOP('',(#29068,#29069,#29070,#29071)) ;
#6057=EDGE_LOOP('',(#29072,#29073,#29074,#29075)) ;
#6058=EDGE_LOOP('',(#29076,#29077,#29078,#29079)) ;
#6059=EDGE_LOOP('',(#29080,#29081,#29082,#29083)) ;
#6060=EDGE_LOOP('',(#29084,#29085,#29086,#29087)) ;
#6061=EDGE_LOOP('',(#29088,#29089,#29090,#29091)) ;
#6062=EDGE_LOOP('',(#29092,#29093,#29094,#29095)) ;
#6063=EDGE_LOOP('',(#29096,#29097,#29098,#29099)) ;
#6064=EDGE_LOOP('',(#29100,#29101,#29102,#29103)) ;
#6065=EDGE_LOOP('',(#29104,#29105,#29106,#29107)) ;
#6066=EDGE_LOOP('',(#29108,#29109,#29110,#29111)) ;
#6067=EDGE_LOOP('',(#29112,#29113,#29114,#29115)) ;
#6068=EDGE_LOOP('',(#29116,#29117,#29118,#29119)) ;
#6069=EDGE_LOOP('',(#29120,#29121,#29122,#29123)) ;
#6070=EDGE_LOOP('',(#29124,#29125,#29126,#29127)) ;
#6071=EDGE_LOOP('',(#29128,#29129,#29130)) ;
#6072=EDGE_LOOP('',(#29131,#29132,#29133,#29134)) ;
#6073=EDGE_LOOP('',(#29135,#29136,#29137)) ;
#6074=EDGE_LOOP('',(#29138,#29139,#29140,#29141)) ;
#6075=EDGE_LOOP('',(#29142,#29143,#29144,#29145)) ;
#6076=EDGE_LOOP('',(#29146,#29147,#29148,#29149)) ;
#6077=EDGE_LOOP('',(#29150,#29151,#29152,#29153)) ;
#6078=EDGE_LOOP('',(#29154,#29155,#29156)) ;
#6079=EDGE_LOOP('',(#29157,#29158,#29159,#29160)) ;
#6080=EDGE_LOOP('',(#29161,#29162,#29163)) ;
#6081=EDGE_LOOP('',(#29164,#29165,#29166,#29167)) ;
#6082=EDGE_LOOP('',(#29168,#29169,#29170,#29171)) ;
#6083=EDGE_LOOP('',(#29172,#29173,#29174,#29175)) ;
#6084=EDGE_LOOP('',(#29176,#29177,#29178,#29179)) ;
#6085=EDGE_LOOP('',(#29180,#29181,#29182)) ;
#6086=EDGE_LOOP('',(#29183,#29184,#29185,#29186)) ;
#6087=EDGE_LOOP('',(#29187,#29188,#29189)) ;
#6088=EDGE_LOOP('',(#29190,#29191,#29192,#29193)) ;
#6089=EDGE_LOOP('',(#29194,#29195,#29196,#29197)) ;
#6090=EDGE_LOOP('',(#29198,#29199,#29200,#29201)) ;
#6091=EDGE_LOOP('',(#29202,#29203,#29204,#29205)) ;
#6092=EDGE_LOOP('',(#29206,#29207,#29208)) ;
#6093=EDGE_LOOP('',(#29209,#29210,#29211,#29212)) ;
#6094=EDGE_LOOP('',(#29213,#29214,#29215)) ;
#6095=EDGE_LOOP('',(#29216,#29217,#29218,#29219)) ;
#6096=EDGE_LOOP('',(#29220,#29221,#29222,#29223)) ;
#6097=EDGE_LOOP('',(#29224,#29225,#29226,#29227)) ;
#6098=EDGE_LOOP('',(#29228,#29229,#29230,#29231,#29232,#29233,#29234,#29235,
#29236,#29237,#29238,#29239,#29240,#29241,#29242,#29243,#29244,#29245,#29246,
#29247,#29248,#29249)) ;
#6099=EDGE_LOOP('',(#29250,#29251,#29252,#29253,#29254,#29255,#29256,#29257,
#29258,#29259,#29260,#29261,#29262,#29263,#29264,#29265,#29266,#29267,#29268,
#29269,#29270,#29271)) ;
#6100=EDGE_LOOP('',(#29272,#29273,#29274,#29275,#29276,#29277,#29278,#29279,
#29280,#29281,#29282,#29283,#29284,#29285,#29286,#29287,#29288,#29289,#29290,
#29291,#29292,#29293)) ;
#6101=EDGE_LOOP('',(#29294,#29295,#29296,#29297,#29298,#29299,#29300,#29301,
#29302,#29303,#29304,#29305,#29306,#29307,#29308,#29309,#29310,#29311,#29312,
#29313,#29314,#29315)) ;
#6102=EDGE_LOOP('',(#29316,#29317,#29318,#29319,#29320,#29321,#29322,#29323,
#29324,#29325,#29326,#29327,#29328,#29329,#29330,#29331,#29332,#29333,#29334,
#29335,#29336,#29337,#29338,#29339,#29340)) ;
#6103=EDGE_LOOP('',(#29341)) ;
#6104=EDGE_LOOP('',(#29342,#29343,#29344,#29345)) ;
#6105=EDGE_LOOP('',(#29346,#29347,#29348)) ;
#6106=EDGE_LOOP('',(#29349,#29350,#29351)) ;
#6107=EDGE_LOOP('',(#29352,#29353,#29354,#29355)) ;
#6108=EDGE_LOOP('',(#29356,#29357,#29358)) ;
#6109=EDGE_LOOP('',(#29359,#29360,#29361)) ;
#6110=EDGE_LOOP('',(#29362,#29363,#29364,#29365)) ;
#6111=EDGE_LOOP('',(#29366,#29367,#29368,#29369)) ;
#6112=EDGE_LOOP('',(#29370,#29371,#29372)) ;
#6113=EDGE_LOOP('',(#29373,#29374,#29375)) ;
#6114=EDGE_LOOP('',(#29376,#29377,#29378,#29379)) ;
#6115=EDGE_LOOP('',(#29380,#29381,#29382)) ;
#6116=EDGE_LOOP('',(#29383,#29384,#29385)) ;
#6117=EDGE_LOOP('',(#29386,#29387,#29388,#29389,#29390,#29391,#29392,#29393)) ;
#6118=EDGE_LOOP('',(#29394,#29395,#29396,#29397,#29398,#29399)) ;
#6119=EDGE_LOOP('',(#29400,#29401,#29402,#29403,#29404,#29405)) ;
#6120=EDGE_LOOP('',(#29406,#29407,#29408,#29409,#29410,#29411)) ;
#8296=LINE('',#81023,#10615) ;
#8297=LINE('',#81027,#10616) ;
#8298=LINE('',#81029,#10617) ;
#8299=LINE('',#81033,#10618) ;
#8300=LINE('',#81034,#10619) ;
#8301=LINE('',#81036,#10620) ;
#8302=LINE('',#81038,#10621) ;
#8303=LINE('',#81042,#10622) ;
#8304=LINE('',#81043,#10623) ;
#8305=LINE('',#81045,#10624) ;
#8306=LINE('',#81047,#10625) ;
#8307=LINE('',#81051,#10626) ;
#8308=LINE('',#81052,#10627) ;
#8309=LINE('',#81054,#10628) ;
#8310=LINE('',#81056,#10629) ;
#8311=LINE('',#81060,#10630) ;
#8312=LINE('',#81061,#10631) ;
#8313=LINE('',#81065,#10632) ;
#8314=LINE('',#81067,#10633) ;
#8315=LINE('',#81069,#10634) ;
#8316=LINE('',#81074,#10635) ;
#8317=LINE('',#81076,#10636) ;
#8318=LINE('',#81079,#10637) ;
#8319=LINE('',#81083,#10638) ;
#8320=LINE('',#81085,#10639) ;
#8321=LINE('',#81087,#10640) ;
#8322=LINE('',#81092,#10641) ;
#8323=LINE('',#81094,#10642) ;
#8324=LINE('',#81097,#10643) ;
#8325=LINE('',#81106,#10644) ;
#8326=LINE('',#81111,#10645) ;
#8327=LINE('',#81120,#10646) ;
#8328=LINE('',#81125,#10647) ;
#8329=LINE('',#81134,#10648) ;
#8330=LINE('',#81139,#10649) ;
#8331=LINE('',#81143,#10650) ;
#8332=LINE('',#81144,#10651) ;
#8333=LINE('',#81145,#10652) ;
#8334=LINE('',#81149,#10653) ;
#8335=LINE('',#81150,#10654) ;
#8336=LINE('',#81151,#10655) ;
#8337=LINE('',#81164,#10656) ;
#8338=LINE('',#81166,#10657) ;
#8339=LINE('',#81168,#10658) ;
#8340=LINE('',#81169,#10659) ;
#8341=LINE('',#81173,#10660) ;
#8342=LINE('',#81175,#10661) ;
#8343=LINE('',#81177,#10662) ;
#8344=LINE('',#81178,#10663) ;
#8345=LINE('',#81190,#10664) ;
#8346=LINE('',#81191,#10665) ;
#8347=LINE('',#81192,#10666) ;
#8348=LINE('',#81196,#10667) ;
#8349=LINE('',#81197,#10668) ;
#8350=LINE('',#81198,#10669) ;
#8351=LINE('',#81211,#10670) ;
#8352=LINE('',#81212,#10671) ;
#8353=LINE('',#81213,#10672) ;
#8354=LINE('',#81217,#10673) ;
#8355=LINE('',#81218,#10674) ;
#8356=LINE('',#81219,#10675) ;
#8357=LINE('',#81243,#10676) ;
#8358=LINE('',#81245,#10677) ;
#8359=LINE('',#81246,#10678) ;
#8360=LINE('',#81250,#10679) ;
#8361=LINE('',#81252,#10680) ;
#8362=LINE('',#81253,#10681) ;
#8363=LINE('',#81257,#10682) ;
#8364=LINE('',#81259,#10683) ;
#8365=LINE('',#81261,#10684) ;
#8366=LINE('',#81262,#10685) ;
#8367=LINE('',#81278,#10686) ;
#8368=LINE('',#81280,#10687) ;
#8369=LINE('',#81281,#10688) ;
#8370=LINE('',#81285,#10689) ;
#8371=LINE('',#81287,#10690) ;
#8372=LINE('',#81288,#10691) ;
#8373=LINE('',#81292,#10692) ;
#8374=LINE('',#81294,#10693) ;
#8375=LINE('',#81296,#10694) ;
#8376=LINE('',#81297,#10695) ;
#8377=LINE('',#81311,#10696) ;
#8378=LINE('',#81313,#10697) ;
#8379=LINE('',#81315,#10698) ;
#8380=LINE('',#81320,#10699) ;
#8381=LINE('',#81322,#10700) ;
#8382=LINE('',#81323,#10701) ;
#8383=LINE('',#81327,#10702) ;
#8384=LINE('',#81329,#10703) ;
#8385=LINE('',#81331,#10704) ;
#8386=LINE('',#81332,#10705) ;
#8387=LINE('',#81346,#10706) ;
#8388=LINE('',#81348,#10707) ;
#8389=LINE('',#81350,#10708) ;
#8390=LINE('',#81355,#10709) ;
#8391=LINE('',#81357,#10710) ;
#8392=LINE('',#81358,#10711) ;
#8393=LINE('',#81362,#10712) ;
#8394=LINE('',#81364,#10713) ;
#8395=LINE('',#81366,#10714) ;
#8396=LINE('',#81367,#10715) ;
#8397=LINE('',#81380,#10716) ;
#8398=LINE('',#81382,#10717) ;
#8399=LINE('',#81384,#10718) ;
#8400=LINE('',#81385,#10719) ;
#8401=LINE('',#81387,#10720) ;
#8402=LINE('',#81388,#10721) ;
#8403=LINE('',#81391,#10722) ;
#8404=LINE('',#81393,#10723) ;
#8405=LINE('',#81395,#10724) ;
#8406=LINE('',#81396,#10725) ;
#8407=LINE('',#81398,#10726) ;
#8408=LINE('',#81399,#10727) ;
#8409=LINE('',#81402,#10728) ;
#8410=LINE('',#81404,#10729) ;
#8411=LINE('',#81406,#10730) ;
#8412=LINE('',#81407,#10731) ;
#8413=LINE('',#81409,#10732) ;
#8414=LINE('',#81410,#10733) ;
#8415=LINE('',#81413,#10734) ;
#8416=LINE('',#81415,#10735) ;
#8417=LINE('',#81417,#10736) ;
#8418=LINE('',#81418,#10737) ;
#8419=LINE('',#81420,#10738) ;
#8420=LINE('',#81421,#10739) ;
#8421=LINE('',#81472,#10740) ;
#8422=LINE('',#81474,#10741) ;
#8423=LINE('',#81518,#10742) ;
#8424=LINE('',#81520,#10743) ;
#8425=LINE('',#81597,#10744) ;
#8426=LINE('',#81599,#10745) ;
#8427=LINE('',#81643,#10746) ;
#8428=LINE('',#81645,#10747) ;
#10615=VECTOR('',#45356,1.651) ;
#10616=VECTOR('',#45361,6.35) ;
#10617=VECTOR('',#45362,6.35) ;
#10618=VECTOR('',#45365,6.35) ;
#10619=VECTOR('',#45366,6.35) ;
#10620=VECTOR('',#45367,6.35) ;
#10621=VECTOR('',#45368,6.35) ;
#10622=VECTOR('',#45371,6.35) ;
#10623=VECTOR('',#45372,6.35) ;
#10624=VECTOR('',#45373,6.35) ;
#10625=VECTOR('',#45374,6.35) ;
#10626=VECTOR('',#45377,6.35) ;
#10627=VECTOR('',#45378,6.35) ;
#10628=VECTOR('',#45379,6.35) ;
#10629=VECTOR('',#45380,6.35) ;
#10630=VECTOR('',#45383,6.35) ;
#10631=VECTOR('',#45384,6.35) ;
#10632=VECTOR('',#45387,6.35) ;
#10633=VECTOR('',#45388,6.35) ;
#10634=VECTOR('',#45389,6.35) ;
#10635=VECTOR('',#45394,6.35) ;
#10636=VECTOR('',#45395,6.35) ;
#10637=VECTOR('',#45398,6.35) ;
#10638=VECTOR('',#45401,6.35) ;
#10639=VECTOR('',#45402,6.35) ;
#10640=VECTOR('',#45403,6.35) ;
#10641=VECTOR('',#45408,6.35) ;
#10642=VECTOR('',#45409,6.35) ;
#10643=VECTOR('',#45412,6.35) ;
#10644=VECTOR('',#45423,6.35) ;
#10645=VECTOR('',#45430,6.35) ;
#10646=VECTOR('',#45441,6.35) ;
#10647=VECTOR('',#45448,6.35) ;
#10648=VECTOR('',#45459,6.35) ;
#10649=VECTOR('',#45466,6.35) ;
#10650=VECTOR('',#45469,6.35) ;
#10651=VECTOR('',#45470,6.35) ;
#10652=VECTOR('',#45471,6.35) ;
#10653=VECTOR('',#45474,6.35) ;
#10654=VECTOR('',#45475,6.35) ;
#10655=VECTOR('',#45476,6.35) ;
#10656=VECTOR('',#45497,6.35) ;
#10657=VECTOR('',#45498,6.35) ;
#10658=VECTOR('',#45499,6.35) ;
#10659=VECTOR('',#45500,6.35) ;
#10660=VECTOR('',#45503,6.35) ;
#10661=VECTOR('',#45504,6.35) ;
#10662=VECTOR('',#45505,6.35) ;
#10663=VECTOR('',#45506,6.35) ;
#10664=VECTOR('',#45525,6.35) ;
#10665=VECTOR('',#45526,6.35) ;
#10666=VECTOR('',#45527,6.35) ;
#10667=VECTOR('',#45530,6.35) ;
#10668=VECTOR('',#45531,6.35) ;
#10669=VECTOR('',#45532,6.35) ;
#10670=VECTOR('',#45553,6.35) ;
#10671=VECTOR('',#45554,6.35) ;
#10672=VECTOR('',#45555,6.35) ;
#10673=VECTOR('',#45558,6.35) ;
#10674=VECTOR('',#45559,6.35) ;
#10675=VECTOR('',#45560,6.35) ;
#10676=VECTOR('',#45601,6.35) ;
#10677=VECTOR('',#45602,6.35) ;
#10678=VECTOR('',#45603,6.35) ;
#10679=VECTOR('',#45606,6.35) ;
#10680=VECTOR('',#45607,6.35) ;
#10681=VECTOR('',#45608,6.35) ;
#10682=VECTOR('',#45611,6.35) ;
#10683=VECTOR('',#45612,6.35) ;
#10684=VECTOR('',#45613,6.35) ;
#10685=VECTOR('',#45614,6.35) ;
#10686=VECTOR('',#45639,6.35) ;
#10687=VECTOR('',#45640,6.35) ;
#10688=VECTOR('',#45641,6.35) ;
#10689=VECTOR('',#45644,6.35) ;
#10690=VECTOR('',#45645,6.35) ;
#10691=VECTOR('',#45646,6.35) ;
#10692=VECTOR('',#45649,6.35) ;
#10693=VECTOR('',#45650,6.35) ;
#10694=VECTOR('',#45651,6.35) ;
#10695=VECTOR('',#45652,6.35) ;
#10696=VECTOR('',#45675,6.35) ;
#10697=VECTOR('',#45676,6.35) ;
#10698=VECTOR('',#45677,6.35) ;
#10699=VECTOR('',#45682,6.35) ;
#10700=VECTOR('',#45683,6.35) ;
#10701=VECTOR('',#45684,6.35) ;
#10702=VECTOR('',#45687,6.35) ;
#10703=VECTOR('',#45688,6.35) ;
#10704=VECTOR('',#45689,6.35) ;
#10705=VECTOR('',#45690,6.35) ;
#10706=VECTOR('',#45713,6.35) ;
#10707=VECTOR('',#45714,6.35) ;
#10708=VECTOR('',#45715,6.35) ;
#10709=VECTOR('',#45720,6.35) ;
#10710=VECTOR('',#45721,6.35) ;
#10711=VECTOR('',#45722,6.35) ;
#10712=VECTOR('',#45725,6.35) ;
#10713=VECTOR('',#45726,6.35) ;
#10714=VECTOR('',#45727,6.35) ;
#10715=VECTOR('',#45728,6.35) ;
#10716=VECTOR('',#45751,6.35) ;
#10717=VECTOR('',#45752,6.35) ;
#10718=VECTOR('',#45753,6.35) ;
#10719=VECTOR('',#45754,6.35) ;
#10720=VECTOR('',#45755,6.35) ;
#10721=VECTOR('',#45756,6.35) ;
#10722=VECTOR('',#45759,6.35) ;
#10723=VECTOR('',#45760,6.35) ;
#10724=VECTOR('',#45761,6.35) ;
#10725=VECTOR('',#45762,6.35) ;
#10726=VECTOR('',#45763,6.35) ;
#10727=VECTOR('',#45764,6.35) ;
#10728=VECTOR('',#45767,6.35) ;
#10729=VECTOR('',#45768,6.35) ;
#10730=VECTOR('',#45769,6.35) ;
#10731=VECTOR('',#45770,6.35) ;
#10732=VECTOR('',#45771,6.35) ;
#10733=VECTOR('',#45772,6.35) ;
#10734=VECTOR('',#45775,6.35) ;
#10735=VECTOR('',#45776,6.35) ;
#10736=VECTOR('',#45777,6.35) ;
#10737=VECTOR('',#45778,6.35) ;
#10738=VECTOR('',#45779,6.35) ;
#10739=VECTOR('',#45780,6.35) ;
#10740=VECTOR('',#45797,6.35) ;
#10741=VECTOR('',#45800,6.35) ;
#10742=VECTOR('',#45805,6.35) ;
#10743=VECTOR('',#45808,6.35) ;
#10744=VECTOR('',#45815,6.35) ;
#10745=VECTOR('',#45818,6.35) ;
#10746=VECTOR('',#45823,6.35) ;
#10747=VECTOR('',#45826,6.35) ;
#12511=CIRCLE('',#36145,4.75315367264104) ;
#12512=CIRCLE('',#36146,5.22940380210988) ;
#12513=CIRCLE('',#36147,4.75315367264148) ;
#12514=CIRCLE('',#36148,5.22940367264214) ;
#12515=CIRCLE('',#36149,4.75315367264191) ;
#12516=CIRCLE('',#36150,5.22940354317232) ;
#12517=CIRCLE('',#36151,4.75315367264155) ;
#12518=CIRCLE('',#36152,5.22940367264084) ;
#12519=CIRCLE('',#36153,4.75315367264153) ;
#12520=CIRCLE('',#36154,5.22940367264213) ;
#12521=CIRCLE('',#36156,1.651) ;
#12522=CIRCLE('',#36157,1.651) ;
#12523=CIRCLE('',#36159,0.730250002314184) ;
#12524=CIRCLE('',#36160,0.730250002314185) ;
#12525=CIRCLE('',#36161,0.730250002314184) ;
#12526=CIRCLE('',#36162,0.730250002314185) ;
#12527=CIRCLE('',#36164,0.571500002304898) ;
#12528=CIRCLE('',#36166,0.571500002304899) ;
#12529=CIRCLE('',#36168,0.571500002304899) ;
#12530=CIRCLE('',#36170,0.571500002304898) ;
#12531=CIRCLE('',#36172,0.0952500014492024) ;
#12532=CIRCLE('',#36173,0.0952500013168486) ;
#12533=CIRCLE('',#36174,0.635) ;
#12534=CIRCLE('',#36176,0.095249999999996) ;
#12535=CIRCLE('',#36178,0.095249999999998) ;
#12536=CIRCLE('',#36180,0.095250001316849) ;
#12537=CIRCLE('',#36181,0.0952500013168486) ;
#12538=CIRCLE('',#36182,0.635) ;
#12539=CIRCLE('',#36184,0.0952499999999976) ;
#12540=CIRCLE('',#36186,0.0952499999999994) ;
#12541=CIRCLE('',#36188,0.0952500014492024) ;
#12542=CIRCLE('',#36189,0.0952500013168531) ;
#12543=CIRCLE('',#36190,0.635) ;
#12544=CIRCLE('',#36192,0.0952499999999996) ;
#12545=CIRCLE('',#36194,0.0952500000000022) ;
#12546=CIRCLE('',#36198,0.635) ;
#12547=CIRCLE('',#36200,0.0634999990163235) ;
#12548=CIRCLE('',#36201,0.0635000000000008) ;
#12549=CIRCLE('',#36203,0.0634999999999982) ;
#12550=CIRCLE('',#36204,0.0634999989174561) ;
#12551=CIRCLE('',#36209,0.0634999990163231) ;
#12552=CIRCLE('',#36210,0.0634999990163244) ;
#12553=CIRCLE('',#36211,0.635) ;
#12554=CIRCLE('',#36213,0.0635000000000008) ;
#12555=CIRCLE('',#36215,0.0634999999999995) ;
#12556=CIRCLE('',#36219,0.635) ;
#12557=CIRCLE('',#36221,0.0634999990163231) ;
#12558=CIRCLE('',#36222,0.0634999990163244) ;
#12559=CIRCLE('',#36224,0.0635000000000008) ;
#12560=CIRCLE('',#36226,0.0635000000000001) ;
#12561=CIRCLE('',#36230,0.635) ;
#12562=CIRCLE('',#36232,0.0634999990163235) ;
#12563=CIRCLE('',#36233,0.0635000000000008) ;
#12564=CIRCLE('',#36235,0.0634999999999985) ;
#12565=CIRCLE('',#36236,0.0634999989174561) ;
#12566=CIRCLE('',#36239,0.635) ;
#12567=CIRCLE('',#36241,0.0952500013168532) ;
#12568=CIRCLE('',#36242,0.0952500013168486) ;
#12569=CIRCLE('',#36244,0.0952500000000016) ;
#12570=CIRCLE('',#36246,0.095249999999998) ;
#12571=CIRCLE('',#36248,0.445135) ;
#12572=CIRCLE('',#36252,0.635000000000001) ;
#12573=CIRCLE('',#36253,0.635) ;
#12574=CIRCLE('',#36255,0.189864999999999) ;
#12575=CIRCLE('',#36256,0.189865) ;
#12576=CIRCLE('',#36258,0.189864999999999) ;
#12577=CIRCLE('',#36259,0.189864999999999) ;
#12578=CIRCLE('',#36262,0.445135) ;
#12579=CIRCLE('',#36266,0.635000000000001) ;
#12580=CIRCLE('',#36267,0.635) ;
#12581=CIRCLE('',#36269,0.189864999999999) ;
#12582=CIRCLE('',#36270,0.189865) ;
#12583=CIRCLE('',#36272,0.189864999999999) ;
#12584=CIRCLE('',#36273,0.189864999999999) ;
#12585=CIRCLE('',#36276,0.445135) ;
#12586=CIRCLE('',#36280,0.635) ;
#12587=CIRCLE('',#36281,0.635) ;
#12588=CIRCLE('',#36283,0.189865) ;
#12589=CIRCLE('',#36284,0.189864999999999) ;
#12590=CIRCLE('',#36286,0.189864999999998) ;
#12591=CIRCLE('',#36287,0.189864999999999) ;
#12592=CIRCLE('',#36290,0.445135) ;
#12593=CIRCLE('',#36294,0.635) ;
#12594=CIRCLE('',#36295,0.635) ;
#12595=CIRCLE('',#36297,0.189864999999999) ;
#12596=CIRCLE('',#36298,0.189864999999999) ;
#12597=CIRCLE('',#36300,0.189864999999998) ;
#12598=CIRCLE('',#36301,0.189864999999999) ;
#12599=CIRCLE('',#36308,4.75315367264138) ;
#12600=CIRCLE('',#36309,4.75315367264185) ;
#12601=CIRCLE('',#36310,4.75315367264196) ;
#12602=CIRCLE('',#36311,4.75315367264146) ;
#12603=CIRCLE('',#36312,4.75315367264139) ;
#12604=CIRCLE('',#36313,5.22940367264163) ;
#12605=CIRCLE('',#36316,5.22940367264085) ;
#12606=CIRCLE('',#36319,5.22940354316612) ;
#12607=CIRCLE('',#36320,5.22940380211795) ;
#12608=CIRCLE('',#36323,5.229403672641) ;
#15264=VERTEX_POINT('',#80831) ;
#15265=VERTEX_POINT('',#80832) ;
#15266=VERTEX_POINT('',#80839) ;
#15267=VERTEX_POINT('',#80841) ;
#15268=VERTEX_POINT('',#80874) ;
#15269=VERTEX_POINT('',#80875) ;
#15270=VERTEX_POINT('',#80882) ;
#15271=VERTEX_POINT('',#80884) ;
#15272=VERTEX_POINT('',#80919) ;
#15273=VERTEX_POINT('',#80921) ;
#15274=VERTEX_POINT('',#80956) ;
#15275=VERTEX_POINT('',#80957) ;
#15276=VERTEX_POINT('',#80964) ;
#15277=VERTEX_POINT('',#80966) ;
#15278=VERTEX_POINT('',#81001) ;
#15279=VERTEX_POINT('',#81002) ;
#15280=VERTEX_POINT('',#81009) ;
#15281=VERTEX_POINT('',#81011) ;
#15282=VERTEX_POINT('',#81020) ;
#15283=VERTEX_POINT('',#81022) ;
#15284=VERTEX_POINT('',#81026) ;
#15285=VERTEX_POINT('',#81028) ;
#15286=VERTEX_POINT('',#81030) ;
#15287=VERTEX_POINT('',#81032) ;
#15288=VERTEX_POINT('',#81035) ;
#15289=VERTEX_POINT('',#81037) ;
#15290=VERTEX_POINT('',#81039) ;
#15291=VERTEX_POINT('',#81041) ;
#15292=VERTEX_POINT('',#81044) ;
#15293=VERTEX_POINT('',#81046) ;
#15294=VERTEX_POINT('',#81048) ;
#15295=VERTEX_POINT('',#81050) ;
#15296=VERTEX_POINT('',#81053) ;
#15297=VERTEX_POINT('',#81055) ;
#15298=VERTEX_POINT('',#81057) ;
#15299=VERTEX_POINT('',#81059) ;
#15300=VERTEX_POINT('',#81063) ;
#15301=VERTEX_POINT('',#81064) ;
#15302=VERTEX_POINT('',#81066) ;
#15303=VERTEX_POINT('',#81068) ;
#15304=VERTEX_POINT('',#81072) ;
#15305=VERTEX_POINT('',#81073) ;
#15306=VERTEX_POINT('',#81075) ;
#15307=VERTEX_POINT('',#81077) ;
#15308=VERTEX_POINT('',#81081) ;
#15309=VERTEX_POINT('',#81082) ;
#15310=VERTEX_POINT('',#81084) ;
#15311=VERTEX_POINT('',#81086) ;
#15312=VERTEX_POINT('',#81090) ;
#15313=VERTEX_POINT('',#81091) ;
#15314=VERTEX_POINT('',#81093) ;
#15315=VERTEX_POINT('',#81095) ;
#15316=VERTEX_POINT('',#81099) ;
#15317=VERTEX_POINT('',#81101) ;
#15318=VERTEX_POINT('',#81105) ;
#15319=VERTEX_POINT('',#81109) ;
#15320=VERTEX_POINT('',#81113) ;
#15321=VERTEX_POINT('',#81115) ;
#15322=VERTEX_POINT('',#81119) ;
#15323=VERTEX_POINT('',#81123) ;
#15324=VERTEX_POINT('',#81127) ;
#15325=VERTEX_POINT('',#81129) ;
#15326=VERTEX_POINT('',#81133) ;
#15327=VERTEX_POINT('',#81137) ;
#15328=VERTEX_POINT('',#81141) ;
#15329=VERTEX_POINT('',#81142) ;
#15330=VERTEX_POINT('',#81147) ;
#15331=VERTEX_POINT('',#81148) ;
#15332=VERTEX_POINT('',#81162) ;
#15333=VERTEX_POINT('',#81163) ;
#15334=VERTEX_POINT('',#81165) ;
#15335=VERTEX_POINT('',#81167) ;
#15336=VERTEX_POINT('',#81171) ;
#15337=VERTEX_POINT('',#81172) ;
#15338=VERTEX_POINT('',#81174) ;
#15339=VERTEX_POINT('',#81176) ;
#15340=VERTEX_POINT('',#81188) ;
#15341=VERTEX_POINT('',#81189) ;
#15342=VERTEX_POINT('',#81194) ;
#15343=VERTEX_POINT('',#81195) ;
#15344=VERTEX_POINT('',#81209) ;
#15345=VERTEX_POINT('',#81210) ;
#15346=VERTEX_POINT('',#81215) ;
#15347=VERTEX_POINT('',#81216) ;
#15348=VERTEX_POINT('',#81239) ;
#15349=VERTEX_POINT('',#81240) ;
#15350=VERTEX_POINT('',#81242) ;
#15351=VERTEX_POINT('',#81244) ;
#15352=VERTEX_POINT('',#81248) ;
#15353=VERTEX_POINT('',#81249) ;
#15354=VERTEX_POINT('',#81251) ;
#15355=VERTEX_POINT('',#81255) ;
#15356=VERTEX_POINT('',#81256) ;
#15357=VERTEX_POINT('',#81258) ;
#15358=VERTEX_POINT('',#81260) ;
#15359=VERTEX_POINT('',#81274) ;
#15360=VERTEX_POINT('',#81275) ;
#15361=VERTEX_POINT('',#81277) ;
#15362=VERTEX_POINT('',#81279) ;
#15363=VERTEX_POINT('',#81283) ;
#15364=VERTEX_POINT('',#81284) ;
#15365=VERTEX_POINT('',#81286) ;
#15366=VERTEX_POINT('',#81290) ;
#15367=VERTEX_POINT('',#81291) ;
#15368=VERTEX_POINT('',#81293) ;
#15369=VERTEX_POINT('',#81295) ;
#15370=VERTEX_POINT('',#81309) ;
#15371=VERTEX_POINT('',#81310) ;
#15372=VERTEX_POINT('',#81312) ;
#15373=VERTEX_POINT('',#81314) ;
#15374=VERTEX_POINT('',#81318) ;
#15375=VERTEX_POINT('',#81319) ;
#15376=VERTEX_POINT('',#81321) ;
#15377=VERTEX_POINT('',#81325) ;
#15378=VERTEX_POINT('',#81326) ;
#15379=VERTEX_POINT('',#81328) ;
#15380=VERTEX_POINT('',#81330) ;
#15381=VERTEX_POINT('',#81344) ;
#15382=VERTEX_POINT('',#81345) ;
#15383=VERTEX_POINT('',#81347) ;
#15384=VERTEX_POINT('',#81349) ;
#15385=VERTEX_POINT('',#81353) ;
#15386=VERTEX_POINT('',#81354) ;
#15387=VERTEX_POINT('',#81356) ;
#15388=VERTEX_POINT('',#81360) ;
#15389=VERTEX_POINT('',#81361) ;
#15390=VERTEX_POINT('',#81363) ;
#15391=VERTEX_POINT('',#81365) ;
#15392=VERTEX_POINT('',#81379) ;
#15393=VERTEX_POINT('',#81381) ;
#15394=VERTEX_POINT('',#81383) ;
#15395=VERTEX_POINT('',#81386) ;
#15396=VERTEX_POINT('',#81390) ;
#15397=VERTEX_POINT('',#81392) ;
#15398=VERTEX_POINT('',#81394) ;
#15399=VERTEX_POINT('',#81397) ;
#15400=VERTEX_POINT('',#81401) ;
#15401=VERTEX_POINT('',#81403) ;
#15402=VERTEX_POINT('',#81405) ;
#15403=VERTEX_POINT('',#81408) ;
#15404=VERTEX_POINT('',#81412) ;
#15405=VERTEX_POINT('',#81414) ;
#15406=VERTEX_POINT('',#81416) ;
#15407=VERTEX_POINT('',#81419) ;
#15408=VERTEX_POINT('',#81424) ;
#15409=VERTEX_POINT('',#81456) ;
#15410=VERTEX_POINT('',#81457) ;
#15411=VERTEX_POINT('',#81502) ;
#15412=VERTEX_POINT('',#81503) ;
#15413=VERTEX_POINT('',#81548) ;
#15414=VERTEX_POINT('',#81549) ;
#15415=VERTEX_POINT('',#81588) ;
#15416=VERTEX_POINT('',#81627) ;
#15417=VERTEX_POINT('',#81628) ;
#19863=EDGE_CURVE('',#15264,#15265,#1612,.T.) ;
#19864=EDGE_CURVE('',#15266,#15264,#12511,.T.) ;
#19865=EDGE_CURVE('',#15267,#15266,#1613,.T.) ;
#19866=EDGE_CURVE('',#15265,#15267,#12512,.T.) ;
#19867=EDGE_CURVE('',#15268,#15269,#1614,.T.) ;
#19868=EDGE_CURVE('',#15270,#15268,#12513,.T.) ;
#19869=EDGE_CURVE('',#15271,#15270,#1615,.T.) ;
#19870=EDGE_CURVE('',#15269,#15271,#12514,.T.) ;
#19871=EDGE_CURVE('',#15272,#15266,#12515,.T.) ;
#19872=EDGE_CURVE('',#15273,#15272,#1616,.T.) ;
#19873=EDGE_CURVE('',#15267,#15273,#12516,.T.) ;
#19874=EDGE_CURVE('',#15274,#15275,#1617,.T.) ;
#19875=EDGE_CURVE('',#15276,#15274,#12517,.T.) ;
#19876=EDGE_CURVE('',#15277,#15276,#1618,.T.) ;
#19877=EDGE_CURVE('',#15275,#15277,#12518,.T.) ;
#19878=EDGE_CURVE('',#15278,#15279,#1619,.T.) ;
#19879=EDGE_CURVE('',#15280,#15278,#12519,.T.) ;
#19880=EDGE_CURVE('',#15281,#15280,#1620,.T.) ;
#19881=EDGE_CURVE('',#15279,#15281,#12520,.T.) ;
#19882=EDGE_CURVE('',#15282,#15282,#12521,.T.) ;
#19883=EDGE_CURVE('',#15282,#15283,#8296,.T.) ;
#19884=EDGE_CURVE('',#15283,#15283,#12522,.T.) ;
#19885=EDGE_CURVE('',#15284,#15268,#8297,.T.) ;
#19886=EDGE_CURVE('',#15284,#15285,#8298,.T.) ;
#19887=EDGE_CURVE('',#15286,#15285,#12523,.T.) ;
#19888=EDGE_CURVE('',#15286,#15287,#8299,.T.) ;
#19889=EDGE_CURVE('',#15276,#15287,#8300,.T.) ;
#19890=EDGE_CURVE('',#15288,#15274,#8301,.T.) ;
#19891=EDGE_CURVE('',#15288,#15289,#8302,.T.) ;
#19892=EDGE_CURVE('',#15290,#15289,#12524,.T.) ;
#19893=EDGE_CURVE('',#15290,#15291,#8303,.T.) ;
#19894=EDGE_CURVE('',#15272,#15291,#8304,.T.) ;
#19895=EDGE_CURVE('',#15292,#15264,#8305,.T.) ;
#19896=EDGE_CURVE('',#15292,#15293,#8306,.T.) ;
#19897=EDGE_CURVE('',#15294,#15293,#12525,.T.) ;
#19898=EDGE_CURVE('',#15294,#15295,#8307,.T.) ;
#19899=EDGE_CURVE('',#15280,#15295,#8308,.T.) ;
#19900=EDGE_CURVE('',#15296,#15278,#8309,.T.) ;
#19901=EDGE_CURVE('',#15296,#15297,#8310,.T.) ;
#19902=EDGE_CURVE('',#15298,#15297,#12526,.T.) ;
#19903=EDGE_CURVE('',#15298,#15299,#8311,.T.) ;
#19904=EDGE_CURVE('',#15270,#15299,#8312,.T.) ;
#19905=EDGE_CURVE('',#15300,#15301,#8313,.T.) ;
#19906=EDGE_CURVE('',#15302,#15300,#8314,.T.) ;
#19907=EDGE_CURVE('',#15303,#15302,#8315,.T.) ;
#19908=EDGE_CURVE('',#15301,#15303,#12527,.T.) ;
#19909=EDGE_CURVE('',#15304,#15305,#8316,.T.) ;
#19910=EDGE_CURVE('',#15306,#15304,#8317,.T.) ;
#19911=EDGE_CURVE('',#15307,#15306,#12528,.T.) ;
#19912=EDGE_CURVE('',#15305,#15307,#8318,.T.) ;
#19913=EDGE_CURVE('',#15308,#15309,#8319,.T.) ;
#19914=EDGE_CURVE('',#15310,#15308,#8320,.T.) ;
#19915=EDGE_CURVE('',#15311,#15310,#8321,.T.) ;
#19916=EDGE_CURVE('',#15309,#15311,#12529,.T.) ;
#19917=EDGE_CURVE('',#15312,#15313,#8322,.T.) ;
#19918=EDGE_CURVE('',#15314,#15312,#8323,.T.) ;
#19919=EDGE_CURVE('',#15315,#15314,#12530,.T.) ;
#19920=EDGE_CURVE('',#15313,#15315,#8324,.T.) ;
#19921=EDGE_CURVE('',#15294,#15316,#12531,.T.) ;
#19922=EDGE_CURVE('',#15293,#15317,#12532,.T.) ;
#19923=EDGE_CURVE('',#15316,#15317,#12533,.T.) ;
#19924=EDGE_CURVE('',#15316,#15318,#8325,.T.) ;
#19925=EDGE_CURVE('',#15295,#15318,#12534,.T.) ;
#19926=EDGE_CURVE('',#15319,#15292,#12535,.T.) ;
#19927=EDGE_CURVE('',#15319,#15317,#8326,.T.) ;
#19928=EDGE_CURVE('',#15320,#15298,#12536,.T.) ;
#19929=EDGE_CURVE('',#15297,#15321,#12537,.T.) ;
#19930=EDGE_CURVE('',#15320,#15321,#12538,.T.) ;
#19931=EDGE_CURVE('',#15320,#15322,#8327,.T.) ;
#19932=EDGE_CURVE('',#15299,#15322,#12539,.T.) ;
#19933=EDGE_CURVE('',#15323,#15296,#12540,.T.) ;
#19934=EDGE_CURVE('',#15323,#15321,#8328,.T.) ;
#19935=EDGE_CURVE('',#15286,#15324,#12541,.T.) ;
#19936=EDGE_CURVE('',#15285,#15325,#12542,.T.) ;
#19937=EDGE_CURVE('',#15324,#15325,#12543,.T.) ;
#19938=EDGE_CURVE('',#15324,#15326,#8329,.T.) ;
#19939=EDGE_CURVE('',#15287,#15326,#12544,.T.) ;
#19940=EDGE_CURVE('',#15327,#15284,#12545,.T.) ;
#19941=EDGE_CURVE('',#15327,#15325,#8330,.T.) ;
#19942=EDGE_CURVE('',#15328,#15329,#8331,.T.) ;
#19943=EDGE_CURVE('',#15326,#15329,#8332,.T.) ;
#19944=EDGE_CURVE('',#15324,#15328,#8333,.T.) ;
#19945=EDGE_CURVE('',#15330,#15331,#8334,.T.) ;
#19946=EDGE_CURVE('',#15325,#15331,#8335,.T.) ;
#19947=EDGE_CURVE('',#15327,#15330,#8336,.T.) ;
#19948=EDGE_CURVE('',#15331,#15328,#12546,.T.) ;
#19949=EDGE_CURVE('',#15311,#15328,#12547,.T.) ;
#19950=EDGE_CURVE('',#15329,#15310,#12548,.T.) ;
#19951=EDGE_CURVE('',#15308,#15330,#12549,.T.) ;
#19952=EDGE_CURVE('',#15309,#15331,#12550,.T.) ;
#19953=EDGE_CURVE('',#15332,#15333,#8337,.T.) ;
#19954=EDGE_CURVE('',#15333,#15334,#8338,.T.) ;
#19955=EDGE_CURVE('',#15335,#15334,#8339,.T.) ;
#19956=EDGE_CURVE('',#15332,#15335,#8340,.T.) ;
#19957=EDGE_CURVE('',#15336,#15337,#8341,.T.) ;
#19958=EDGE_CURVE('',#15337,#15338,#8342,.T.) ;
#19959=EDGE_CURVE('',#15339,#15338,#8343,.T.) ;
#19960=EDGE_CURVE('',#15336,#15339,#8344,.T.) ;
#19961=EDGE_CURVE('',#15338,#15307,#12551,.T.) ;
#19962=EDGE_CURVE('',#15306,#15333,#12552,.T.) ;
#19963=EDGE_CURVE('',#15338,#15333,#12553,.T.) ;
#19964=EDGE_CURVE('',#15334,#15304,#12554,.T.) ;
#19965=EDGE_CURVE('',#15305,#15337,#12555,.T.) ;
#19966=EDGE_CURVE('',#15340,#15341,#8345,.T.) ;
#19967=EDGE_CURVE('',#15318,#15341,#8346,.T.) ;
#19968=EDGE_CURVE('',#15316,#15340,#8347,.T.) ;
#19969=EDGE_CURVE('',#15342,#15343,#8348,.T.) ;
#19970=EDGE_CURVE('',#15317,#15343,#8349,.T.) ;
#19971=EDGE_CURVE('',#15319,#15342,#8350,.T.) ;
#19972=EDGE_CURVE('',#15343,#15340,#12556,.T.) ;
#19973=EDGE_CURVE('',#15343,#15315,#12557,.T.) ;
#19974=EDGE_CURVE('',#15314,#15340,#12558,.T.) ;
#19975=EDGE_CURVE('',#15341,#15312,#12559,.T.) ;
#19976=EDGE_CURVE('',#15313,#15342,#12560,.T.) ;
#19977=EDGE_CURVE('',#15344,#15345,#8351,.T.) ;
#19978=EDGE_CURVE('',#15322,#15345,#8352,.T.) ;
#19979=EDGE_CURVE('',#15320,#15344,#8353,.T.) ;
#19980=EDGE_CURVE('',#15346,#15347,#8354,.T.) ;
#19981=EDGE_CURVE('',#15321,#15347,#8355,.T.) ;
#19982=EDGE_CURVE('',#15323,#15346,#8356,.T.) ;
#19983=EDGE_CURVE('',#15347,#15344,#12561,.T.) ;
#19984=EDGE_CURVE('',#15303,#15344,#12562,.T.) ;
#19985=EDGE_CURVE('',#15345,#15302,#12563,.T.) ;
#19986=EDGE_CURVE('',#15300,#15346,#12564,.T.) ;
#19987=EDGE_CURVE('',#15301,#15347,#12565,.T.) ;
#19988=EDGE_CURVE('',#15332,#15339,#12566,.T.) ;
#19989=EDGE_CURVE('',#15332,#15290,#12567,.T.) ;
#19990=EDGE_CURVE('',#15289,#15339,#12568,.T.) ;
#19991=EDGE_CURVE('',#15291,#15335,#12569,.T.) ;
#19992=EDGE_CURVE('',#15336,#15288,#12570,.T.) ;
#19993=EDGE_CURVE('',#15348,#15349,#12571,.T.) ;
#19994=EDGE_CURVE('',#15349,#15350,#8357,.T.) ;
#19995=EDGE_CURVE('',#15350,#15351,#8358,.T.) ;
#19996=EDGE_CURVE('',#15351,#15348,#8359,.T.) ;
#19997=EDGE_CURVE('',#15352,#15353,#8360,.T.) ;
#19998=EDGE_CURVE('',#15353,#15354,#8361,.T.) ;
#19999=EDGE_CURVE('',#15352,#15354,#8362,.T.) ;
#20000=EDGE_CURVE('',#15355,#15356,#8363,.T.) ;
#20001=EDGE_CURVE('',#15355,#15357,#8364,.T.) ;
#20002=EDGE_CURVE('',#15357,#15358,#8365,.T.) ;
#20003=EDGE_CURVE('',#15356,#15358,#8366,.T.) ;
#20004=EDGE_CURVE('',#15357,#15352,#12572,.T.) ;
#20005=EDGE_CURVE('',#15358,#15352,#12573,.T.) ;
#20006=EDGE_CURVE('',#15350,#15354,#12574,.T.) ;
#20007=EDGE_CURVE('',#15352,#15349,#12575,.T.) ;
#20008=EDGE_CURVE('',#15358,#15348,#12576,.T.) ;
#20009=EDGE_CURVE('',#15356,#15351,#12577,.T.) ;
#20010=EDGE_CURVE('',#15359,#15360,#12578,.T.) ;
#20011=EDGE_CURVE('',#15360,#15361,#8367,.T.) ;
#20012=EDGE_CURVE('',#15361,#15362,#8368,.T.) ;
#20013=EDGE_CURVE('',#15362,#15359,#8369,.T.) ;
#20014=EDGE_CURVE('',#15363,#15364,#8370,.T.) ;
#20015=EDGE_CURVE('',#15364,#15365,#8371,.T.) ;
#20016=EDGE_CURVE('',#15363,#15365,#8372,.T.) ;
#20017=EDGE_CURVE('',#15366,#15367,#8373,.T.) ;
#20018=EDGE_CURVE('',#15366,#15368,#8374,.T.) ;
#20019=EDGE_CURVE('',#15368,#15369,#8375,.T.) ;
#20020=EDGE_CURVE('',#15367,#15369,#8376,.T.) ;
#20021=EDGE_CURVE('',#15368,#15363,#12579,.T.) ;
#20022=EDGE_CURVE('',#15369,#15363,#12580,.T.) ;
#20023=EDGE_CURVE('',#15361,#15365,#12581,.T.) ;
#20024=EDGE_CURVE('',#15363,#15360,#12582,.T.) ;
#20025=EDGE_CURVE('',#15369,#15359,#12583,.T.) ;
#20026=EDGE_CURVE('',#15367,#15362,#12584,.T.) ;
#20027=EDGE_CURVE('',#15370,#15371,#8377,.T.) ;
#20028=EDGE_CURVE('',#15372,#15370,#8378,.T.) ;
#20029=EDGE_CURVE('',#15373,#15372,#8379,.T.) ;
#20030=EDGE_CURVE('',#15371,#15373,#12585,.T.) ;
#20031=EDGE_CURVE('',#15374,#15375,#8380,.T.) ;
#20032=EDGE_CURVE('',#15376,#15375,#8381,.T.) ;
#20033=EDGE_CURVE('',#15376,#15374,#8382,.T.) ;
#20034=EDGE_CURVE('',#15377,#15378,#8383,.T.) ;
#20035=EDGE_CURVE('',#15379,#15378,#8384,.T.) ;
#20036=EDGE_CURVE('',#15379,#15380,#8385,.T.) ;
#20037=EDGE_CURVE('',#15380,#15377,#8386,.T.) ;
#20038=EDGE_CURVE('',#15378,#15374,#12586,.T.) ;
#20039=EDGE_CURVE('',#15374,#15379,#12587,.T.) ;
#20040=EDGE_CURVE('',#15374,#15373,#12588,.T.) ;
#20041=EDGE_CURVE('',#15372,#15375,#12589,.T.) ;
#20042=EDGE_CURVE('',#15377,#15370,#12590,.T.) ;
#20043=EDGE_CURVE('',#15378,#15371,#12591,.T.) ;
#20044=EDGE_CURVE('',#15381,#15382,#8387,.T.) ;
#20045=EDGE_CURVE('',#15383,#15381,#8388,.T.) ;
#20046=EDGE_CURVE('',#15384,#15383,#8389,.T.) ;
#20047=EDGE_CURVE('',#15382,#15384,#12592,.T.) ;
#20048=EDGE_CURVE('',#15385,#15386,#8390,.T.) ;
#20049=EDGE_CURVE('',#15387,#15386,#8391,.T.) ;
#20050=EDGE_CURVE('',#15387,#15385,#8392,.T.) ;
#20051=EDGE_CURVE('',#15388,#15389,#8393,.T.) ;
#20052=EDGE_CURVE('',#15390,#15389,#8394,.T.) ;
#20053=EDGE_CURVE('',#15390,#15391,#8395,.T.) ;
#20054=EDGE_CURVE('',#15391,#15388,#8396,.T.) ;
#20055=EDGE_CURVE('',#15389,#15385,#12593,.T.) ;
#20056=EDGE_CURVE('',#15385,#15390,#12594,.T.) ;
#20057=EDGE_CURVE('',#15385,#15384,#12595,.T.) ;
#20058=EDGE_CURVE('',#15383,#15386,#12596,.T.) ;
#20059=EDGE_CURVE('',#15388,#15381,#12597,.T.) ;
#20060=EDGE_CURVE('',#15389,#15382,#12598,.T.) ;
#20061=EDGE_CURVE('',#15392,#15271,#8397,.T.) ;
#20062=EDGE_CURVE('',#15279,#15393,#8398,.T.) ;
#20063=EDGE_CURVE('',#15394,#15393,#8399,.T.) ;
#20064=EDGE_CURVE('',#15355,#15394,#8400,.T.) ;
#20065=EDGE_CURVE('',#15395,#15353,#8401,.T.) ;
#20066=EDGE_CURVE('',#15392,#15395,#8402,.T.) ;
#20067=EDGE_CURVE('',#15396,#15273,#8403,.T.) ;
#20068=EDGE_CURVE('',#15275,#15397,#8404,.T.) ;
#20069=EDGE_CURVE('',#15398,#15397,#8405,.T.) ;
#20070=EDGE_CURVE('',#15387,#15398,#8406,.T.) ;
#20071=EDGE_CURVE('',#15399,#15391,#8407,.T.) ;
#20072=EDGE_CURVE('',#15396,#15399,#8408,.T.) ;
#20073=EDGE_CURVE('',#15400,#15277,#8409,.T.) ;
#20074=EDGE_CURVE('',#15269,#15401,#8410,.T.) ;
#20075=EDGE_CURVE('',#15402,#15401,#8411,.T.) ;
#20076=EDGE_CURVE('',#15366,#15402,#8412,.T.) ;
#20077=EDGE_CURVE('',#15403,#15364,#8413,.T.) ;
#20078=EDGE_CURVE('',#15400,#15403,#8414,.T.) ;
#20079=EDGE_CURVE('',#15404,#15281,#8415,.T.) ;
#20080=EDGE_CURVE('',#15265,#15405,#8416,.T.) ;
#20081=EDGE_CURVE('',#15406,#15405,#8417,.T.) ;
#20082=EDGE_CURVE('',#15376,#15406,#8418,.T.) ;
#20083=EDGE_CURVE('',#15407,#15380,#8419,.T.) ;
#20084=EDGE_CURVE('',#15404,#15407,#8420,.T.) ;
#20085=EDGE_CURVE('',#15407,#15394,#12599,.T.) ;
#20086=EDGE_CURVE('',#15408,#15406,#12600,.T.) ;
#20087=EDGE_CURVE('',#15399,#15408,#12601,.T.) ;
#20088=EDGE_CURVE('',#15403,#15398,#12602,.T.) ;
#20089=EDGE_CURVE('',#15395,#15402,#12603,.T.) ;
#20090=EDGE_CURVE('',#15409,#15410,#12604,.T.) ;
#20091=EDGE_CURVE('',#15410,#15395,#1621,.T.) ;
#20092=EDGE_CURVE('',#15402,#15409,#1622,.T.) ;
#20093=EDGE_CURVE('',#15410,#15392,#8421,.T.) ;
#20094=EDGE_CURVE('',#15401,#15409,#8422,.T.) ;
#20095=EDGE_CURVE('',#15411,#15412,#12605,.T.) ;
#20096=EDGE_CURVE('',#15412,#15403,#1623,.T.) ;
#20097=EDGE_CURVE('',#15398,#15411,#1624,.T.) ;
#20098=EDGE_CURVE('',#15397,#15411,#8423,.T.) ;
#20099=EDGE_CURVE('',#15412,#15400,#8424,.T.) ;
#20100=EDGE_CURVE('',#15413,#15414,#12606,.T.) ;
#20101=EDGE_CURVE('',#15414,#15399,#1625,.T.) ;
#20102=EDGE_CURVE('',#15413,#15408,#1626,.T.) ;
#20103=EDGE_CURVE('',#15415,#15413,#12607,.T.) ;
#20104=EDGE_CURVE('',#15406,#15415,#1627,.T.) ;
#20105=EDGE_CURVE('',#15414,#15396,#8425,.T.) ;
#20106=EDGE_CURVE('',#15405,#15415,#8426,.T.) ;
#20107=EDGE_CURVE('',#15416,#15417,#12608,.T.) ;
#20108=EDGE_CURVE('',#15417,#15407,#1628,.T.) ;
#20109=EDGE_CURVE('',#15394,#15416,#1629,.T.) ;
#20110=EDGE_CURVE('',#15393,#15416,#8427,.T.) ;
#20111=EDGE_CURVE('',#15417,#15404,#8428,.T.) ;
#28914=ORIENTED_EDGE('',*,*,#19863,.F.) ;
#28915=ORIENTED_EDGE('',*,*,#19864,.F.) ;
#28916=ORIENTED_EDGE('',*,*,#19865,.F.) ;
#28917=ORIENTED_EDGE('',*,*,#19866,.F.) ;
#28918=ORIENTED_EDGE('',*,*,#19867,.F.) ;
#28919=ORIENTED_EDGE('',*,*,#19868,.F.) ;
#28920=ORIENTED_EDGE('',*,*,#19869,.F.) ;
#28921=ORIENTED_EDGE('',*,*,#19870,.F.) ;
#28922=ORIENTED_EDGE('',*,*,#19865,.T.) ;
#28923=ORIENTED_EDGE('',*,*,#19871,.F.) ;
#28924=ORIENTED_EDGE('',*,*,#19872,.F.) ;
#28925=ORIENTED_EDGE('',*,*,#19873,.F.) ;
#28926=ORIENTED_EDGE('',*,*,#19874,.F.) ;
#28927=ORIENTED_EDGE('',*,*,#19875,.F.) ;
#28928=ORIENTED_EDGE('',*,*,#19876,.F.) ;
#28929=ORIENTED_EDGE('',*,*,#19877,.F.) ;
#28930=ORIENTED_EDGE('',*,*,#19878,.F.) ;
#28931=ORIENTED_EDGE('',*,*,#19879,.F.) ;
#28932=ORIENTED_EDGE('',*,*,#19880,.F.) ;
#28933=ORIENTED_EDGE('',*,*,#19881,.F.) ;
#28934=ORIENTED_EDGE('',*,*,#19882,.F.) ;
#28935=ORIENTED_EDGE('',*,*,#19883,.T.) ;
#28936=ORIENTED_EDGE('',*,*,#19884,.T.) ;
#28937=ORIENTED_EDGE('',*,*,#19883,.F.) ;
#28938=ORIENTED_EDGE('',*,*,#19868,.T.) ;
#28939=ORIENTED_EDGE('',*,*,#19885,.F.) ;
#28940=ORIENTED_EDGE('',*,*,#19886,.T.) ;
#28941=ORIENTED_EDGE('',*,*,#19887,.F.) ;
#28942=ORIENTED_EDGE('',*,*,#19888,.T.) ;
#28943=ORIENTED_EDGE('',*,*,#19889,.F.) ;
#28944=ORIENTED_EDGE('',*,*,#19875,.T.) ;
#28945=ORIENTED_EDGE('',*,*,#19890,.F.) ;
#28946=ORIENTED_EDGE('',*,*,#19891,.T.) ;
#28947=ORIENTED_EDGE('',*,*,#19892,.F.) ;
#28948=ORIENTED_EDGE('',*,*,#19893,.T.) ;
#28949=ORIENTED_EDGE('',*,*,#19894,.F.) ;
#28950=ORIENTED_EDGE('',*,*,#19871,.T.) ;
#28951=ORIENTED_EDGE('',*,*,#19864,.T.) ;
#28952=ORIENTED_EDGE('',*,*,#19895,.F.) ;
#28953=ORIENTED_EDGE('',*,*,#19896,.T.) ;
#28954=ORIENTED_EDGE('',*,*,#19897,.F.) ;
#28955=ORIENTED_EDGE('',*,*,#19898,.T.) ;
#28956=ORIENTED_EDGE('',*,*,#19899,.F.) ;
#28957=ORIENTED_EDGE('',*,*,#19879,.T.) ;
#28958=ORIENTED_EDGE('',*,*,#19900,.F.) ;
#28959=ORIENTED_EDGE('',*,*,#19901,.T.) ;
#28960=ORIENTED_EDGE('',*,*,#19902,.F.) ;
#28961=ORIENTED_EDGE('',*,*,#19903,.T.) ;
#28962=ORIENTED_EDGE('',*,*,#19904,.F.) ;
#28963=ORIENTED_EDGE('',*,*,#19882,.T.) ;
#28964=ORIENTED_EDGE('',*,*,#19905,.F.) ;
#28965=ORIENTED_EDGE('',*,*,#19906,.F.) ;
#28966=ORIENTED_EDGE('',*,*,#19907,.F.) ;
#28967=ORIENTED_EDGE('',*,*,#19908,.F.) ;
#28968=ORIENTED_EDGE('',*,*,#19909,.F.) ;
#28969=ORIENTED_EDGE('',*,*,#19910,.F.) ;
#28970=ORIENTED_EDGE('',*,*,#19911,.F.) ;
#28971=ORIENTED_EDGE('',*,*,#19912,.F.) ;
#28972=ORIENTED_EDGE('',*,*,#19913,.F.) ;
#28973=ORIENTED_EDGE('',*,*,#19914,.F.) ;
#28974=ORIENTED_EDGE('',*,*,#19915,.F.) ;
#28975=ORIENTED_EDGE('',*,*,#19916,.F.) ;
#28976=ORIENTED_EDGE('',*,*,#19917,.F.) ;
#28977=ORIENTED_EDGE('',*,*,#19918,.F.) ;
#28978=ORIENTED_EDGE('',*,*,#19919,.F.) ;
#28979=ORIENTED_EDGE('',*,*,#19920,.F.) ;
#28980=ORIENTED_EDGE('',*,*,#19921,.F.) ;
#28981=ORIENTED_EDGE('',*,*,#19897,.T.) ;
#28982=ORIENTED_EDGE('',*,*,#19922,.T.) ;
#28983=ORIENTED_EDGE('',*,*,#19923,.F.) ;
#28984=ORIENTED_EDGE('',*,*,#19921,.T.) ;
#28985=ORIENTED_EDGE('',*,*,#19924,.T.) ;
#28986=ORIENTED_EDGE('',*,*,#19925,.F.) ;
#28987=ORIENTED_EDGE('',*,*,#19898,.F.) ;
#28988=ORIENTED_EDGE('',*,*,#19926,.F.) ;
#28989=ORIENTED_EDGE('',*,*,#19927,.T.) ;
#28990=ORIENTED_EDGE('',*,*,#19922,.F.) ;
#28991=ORIENTED_EDGE('',*,*,#19896,.F.) ;
#28992=ORIENTED_EDGE('',*,*,#19928,.T.) ;
#28993=ORIENTED_EDGE('',*,*,#19902,.T.) ;
#28994=ORIENTED_EDGE('',*,*,#19929,.T.) ;
#28995=ORIENTED_EDGE('',*,*,#19930,.F.) ;
#28996=ORIENTED_EDGE('',*,*,#19928,.F.) ;
#28997=ORIENTED_EDGE('',*,*,#19931,.T.) ;
#28998=ORIENTED_EDGE('',*,*,#19932,.F.) ;
#28999=ORIENTED_EDGE('',*,*,#19903,.F.) ;
#29000=ORIENTED_EDGE('',*,*,#19933,.F.) ;
#29001=ORIENTED_EDGE('',*,*,#19934,.T.) ;
#29002=ORIENTED_EDGE('',*,*,#19929,.F.) ;
#29003=ORIENTED_EDGE('',*,*,#19901,.F.) ;
#29004=ORIENTED_EDGE('',*,*,#19935,.F.) ;
#29005=ORIENTED_EDGE('',*,*,#19887,.T.) ;
#29006=ORIENTED_EDGE('',*,*,#19936,.T.) ;
#29007=ORIENTED_EDGE('',*,*,#19937,.F.) ;
#29008=ORIENTED_EDGE('',*,*,#19935,.T.) ;
#29009=ORIENTED_EDGE('',*,*,#19938,.T.) ;
#29010=ORIENTED_EDGE('',*,*,#19939,.F.) ;
#29011=ORIENTED_EDGE('',*,*,#19888,.F.) ;
#29012=ORIENTED_EDGE('',*,*,#19940,.F.) ;
#29013=ORIENTED_EDGE('',*,*,#19941,.T.) ;
#29014=ORIENTED_EDGE('',*,*,#19936,.F.) ;
#29015=ORIENTED_EDGE('',*,*,#19886,.F.) ;
#29016=ORIENTED_EDGE('',*,*,#19942,.T.) ;
#29017=ORIENTED_EDGE('',*,*,#19943,.F.) ;
#29018=ORIENTED_EDGE('',*,*,#19938,.F.) ;
#29019=ORIENTED_EDGE('',*,*,#19944,.T.) ;
#29020=ORIENTED_EDGE('',*,*,#19945,.T.) ;
#29021=ORIENTED_EDGE('',*,*,#19946,.F.) ;
#29022=ORIENTED_EDGE('',*,*,#19941,.F.) ;
#29023=ORIENTED_EDGE('',*,*,#19947,.T.) ;
#29024=ORIENTED_EDGE('',*,*,#19948,.T.) ;
#29025=ORIENTED_EDGE('',*,*,#19944,.F.) ;
#29026=ORIENTED_EDGE('',*,*,#19937,.T.) ;
#29027=ORIENTED_EDGE('',*,*,#19946,.T.) ;
#29028=ORIENTED_EDGE('',*,*,#19949,.F.) ;
#29029=ORIENTED_EDGE('',*,*,#19915,.T.) ;
#29030=ORIENTED_EDGE('',*,*,#19950,.F.) ;
#29031=ORIENTED_EDGE('',*,*,#19942,.F.) ;
#29032=ORIENTED_EDGE('',*,*,#19951,.F.) ;
#29033=ORIENTED_EDGE('',*,*,#19913,.T.) ;
#29034=ORIENTED_EDGE('',*,*,#19952,.T.) ;
#29035=ORIENTED_EDGE('',*,*,#19945,.F.) ;
#29036=ORIENTED_EDGE('',*,*,#19952,.F.) ;
#29037=ORIENTED_EDGE('',*,*,#19916,.T.) ;
#29038=ORIENTED_EDGE('',*,*,#19949,.T.) ;
#29039=ORIENTED_EDGE('',*,*,#19948,.F.) ;
#29040=ORIENTED_EDGE('',*,*,#19953,.T.) ;
#29041=ORIENTED_EDGE('',*,*,#19954,.T.) ;
#29042=ORIENTED_EDGE('',*,*,#19955,.F.) ;
#29043=ORIENTED_EDGE('',*,*,#19956,.F.) ;
#29044=ORIENTED_EDGE('',*,*,#19957,.T.) ;
#29045=ORIENTED_EDGE('',*,*,#19958,.T.) ;
#29046=ORIENTED_EDGE('',*,*,#19959,.F.) ;
#29047=ORIENTED_EDGE('',*,*,#19960,.F.) ;
#29048=ORIENTED_EDGE('',*,*,#19961,.T.) ;
#29049=ORIENTED_EDGE('',*,*,#19911,.T.) ;
#29050=ORIENTED_EDGE('',*,*,#19962,.T.) ;
#29051=ORIENTED_EDGE('',*,*,#19963,.F.) ;
#29052=ORIENTED_EDGE('',*,*,#19962,.F.) ;
#29053=ORIENTED_EDGE('',*,*,#19910,.T.) ;
#29054=ORIENTED_EDGE('',*,*,#19964,.F.) ;
#29055=ORIENTED_EDGE('',*,*,#19954,.F.) ;
#29056=ORIENTED_EDGE('',*,*,#19965,.F.) ;
#29057=ORIENTED_EDGE('',*,*,#19912,.T.) ;
#29058=ORIENTED_EDGE('',*,*,#19961,.F.) ;
#29059=ORIENTED_EDGE('',*,*,#19958,.F.) ;
#29060=ORIENTED_EDGE('',*,*,#19966,.T.) ;
#29061=ORIENTED_EDGE('',*,*,#19967,.F.) ;
#29062=ORIENTED_EDGE('',*,*,#19924,.F.) ;
#29063=ORIENTED_EDGE('',*,*,#19968,.T.) ;
#29064=ORIENTED_EDGE('',*,*,#19969,.T.) ;
#29065=ORIENTED_EDGE('',*,*,#19970,.F.) ;
#29066=ORIENTED_EDGE('',*,*,#19927,.F.) ;
#29067=ORIENTED_EDGE('',*,*,#19971,.T.) ;
#29068=ORIENTED_EDGE('',*,*,#19972,.T.) ;
#29069=ORIENTED_EDGE('',*,*,#19968,.F.) ;
#29070=ORIENTED_EDGE('',*,*,#19923,.T.) ;
#29071=ORIENTED_EDGE('',*,*,#19970,.T.) ;
#29072=ORIENTED_EDGE('',*,*,#19973,.T.) ;
#29073=ORIENTED_EDGE('',*,*,#19919,.T.) ;
#29074=ORIENTED_EDGE('',*,*,#19974,.T.) ;
#29075=ORIENTED_EDGE('',*,*,#19972,.F.) ;
#29076=ORIENTED_EDGE('',*,*,#19974,.F.) ;
#29077=ORIENTED_EDGE('',*,*,#19918,.T.) ;
#29078=ORIENTED_EDGE('',*,*,#19975,.F.) ;
#29079=ORIENTED_EDGE('',*,*,#19966,.F.) ;
#29080=ORIENTED_EDGE('',*,*,#19976,.F.) ;
#29081=ORIENTED_EDGE('',*,*,#19920,.T.) ;
#29082=ORIENTED_EDGE('',*,*,#19973,.F.) ;
#29083=ORIENTED_EDGE('',*,*,#19969,.F.) ;
#29084=ORIENTED_EDGE('',*,*,#19977,.T.) ;
#29085=ORIENTED_EDGE('',*,*,#19978,.F.) ;
#29086=ORIENTED_EDGE('',*,*,#19931,.F.) ;
#29087=ORIENTED_EDGE('',*,*,#19979,.T.) ;
#29088=ORIENTED_EDGE('',*,*,#19980,.T.) ;
#29089=ORIENTED_EDGE('',*,*,#19981,.F.) ;
#29090=ORIENTED_EDGE('',*,*,#19934,.F.) ;
#29091=ORIENTED_EDGE('',*,*,#19982,.T.) ;
#29092=ORIENTED_EDGE('',*,*,#19983,.T.) ;
#29093=ORIENTED_EDGE('',*,*,#19979,.F.) ;
#29094=ORIENTED_EDGE('',*,*,#19930,.T.) ;
#29095=ORIENTED_EDGE('',*,*,#19981,.T.) ;
#29096=ORIENTED_EDGE('',*,*,#19984,.F.) ;
#29097=ORIENTED_EDGE('',*,*,#19907,.T.) ;
#29098=ORIENTED_EDGE('',*,*,#19985,.F.) ;
#29099=ORIENTED_EDGE('',*,*,#19977,.F.) ;
#29100=ORIENTED_EDGE('',*,*,#19986,.F.) ;
#29101=ORIENTED_EDGE('',*,*,#19905,.T.) ;
#29102=ORIENTED_EDGE('',*,*,#19987,.T.) ;
#29103=ORIENTED_EDGE('',*,*,#19980,.F.) ;
#29104=ORIENTED_EDGE('',*,*,#19987,.F.) ;
#29105=ORIENTED_EDGE('',*,*,#19908,.T.) ;
#29106=ORIENTED_EDGE('',*,*,#19984,.T.) ;
#29107=ORIENTED_EDGE('',*,*,#19983,.F.) ;
#29108=ORIENTED_EDGE('',*,*,#19988,.T.) ;
#29109=ORIENTED_EDGE('',*,*,#19959,.T.) ;
#29110=ORIENTED_EDGE('',*,*,#19963,.T.) ;
#29111=ORIENTED_EDGE('',*,*,#19953,.F.) ;
#29112=ORIENTED_EDGE('',*,*,#19989,.T.) ;
#29113=ORIENTED_EDGE('',*,*,#19892,.T.) ;
#29114=ORIENTED_EDGE('',*,*,#19990,.T.) ;
#29115=ORIENTED_EDGE('',*,*,#19988,.F.) ;
#29116=ORIENTED_EDGE('',*,*,#19989,.F.) ;
#29117=ORIENTED_EDGE('',*,*,#19956,.T.) ;
#29118=ORIENTED_EDGE('',*,*,#19991,.F.) ;
#29119=ORIENTED_EDGE('',*,*,#19893,.F.) ;
#29120=ORIENTED_EDGE('',*,*,#19992,.F.) ;
#29121=ORIENTED_EDGE('',*,*,#19960,.T.) ;
#29122=ORIENTED_EDGE('',*,*,#19990,.F.) ;
#29123=ORIENTED_EDGE('',*,*,#19891,.F.) ;
#29124=ORIENTED_EDGE('',*,*,#19993,.T.) ;
#29125=ORIENTED_EDGE('',*,*,#19994,.T.) ;
#29126=ORIENTED_EDGE('',*,*,#19995,.T.) ;
#29127=ORIENTED_EDGE('',*,*,#19996,.T.) ;
#29128=ORIENTED_EDGE('',*,*,#19997,.T.) ;
#29129=ORIENTED_EDGE('',*,*,#19998,.T.) ;
#29130=ORIENTED_EDGE('',*,*,#19999,.F.) ;
#29131=ORIENTED_EDGE('',*,*,#20000,.F.) ;
#29132=ORIENTED_EDGE('',*,*,#20001,.T.) ;
#29133=ORIENTED_EDGE('',*,*,#20002,.T.) ;
#29134=ORIENTED_EDGE('',*,*,#20003,.F.) ;
#29135=ORIENTED_EDGE('',*,*,#20002,.F.) ;
#29136=ORIENTED_EDGE('',*,*,#20004,.T.) ;
#29137=ORIENTED_EDGE('',*,*,#20005,.F.) ;
#29138=ORIENTED_EDGE('',*,*,#19999,.T.) ;
#29139=ORIENTED_EDGE('',*,*,#20006,.F.) ;
#29140=ORIENTED_EDGE('',*,*,#19994,.F.) ;
#29141=ORIENTED_EDGE('',*,*,#20007,.F.) ;
#29142=ORIENTED_EDGE('',*,*,#20003,.T.) ;
#29143=ORIENTED_EDGE('',*,*,#20008,.T.) ;
#29144=ORIENTED_EDGE('',*,*,#19996,.F.) ;
#29145=ORIENTED_EDGE('',*,*,#20009,.F.) ;
#29146=ORIENTED_EDGE('',*,*,#20005,.T.) ;
#29147=ORIENTED_EDGE('',*,*,#20007,.T.) ;
#29148=ORIENTED_EDGE('',*,*,#19993,.F.) ;
#29149=ORIENTED_EDGE('',*,*,#20008,.F.) ;
#29150=ORIENTED_EDGE('',*,*,#20010,.T.) ;
#29151=ORIENTED_EDGE('',*,*,#20011,.T.) ;
#29152=ORIENTED_EDGE('',*,*,#20012,.T.) ;
#29153=ORIENTED_EDGE('',*,*,#20013,.T.) ;
#29154=ORIENTED_EDGE('',*,*,#20014,.T.) ;
#29155=ORIENTED_EDGE('',*,*,#20015,.T.) ;
#29156=ORIENTED_EDGE('',*,*,#20016,.F.) ;
#29157=ORIENTED_EDGE('',*,*,#20017,.F.) ;
#29158=ORIENTED_EDGE('',*,*,#20018,.T.) ;
#29159=ORIENTED_EDGE('',*,*,#20019,.T.) ;
#29160=ORIENTED_EDGE('',*,*,#20020,.F.) ;
#29161=ORIENTED_EDGE('',*,*,#20019,.F.) ;
#29162=ORIENTED_EDGE('',*,*,#20021,.T.) ;
#29163=ORIENTED_EDGE('',*,*,#20022,.F.) ;
#29164=ORIENTED_EDGE('',*,*,#20016,.T.) ;
#29165=ORIENTED_EDGE('',*,*,#20023,.F.) ;
#29166=ORIENTED_EDGE('',*,*,#20011,.F.) ;
#29167=ORIENTED_EDGE('',*,*,#20024,.F.) ;
#29168=ORIENTED_EDGE('',*,*,#20020,.T.) ;
#29169=ORIENTED_EDGE('',*,*,#20025,.T.) ;
#29170=ORIENTED_EDGE('',*,*,#20013,.F.) ;
#29171=ORIENTED_EDGE('',*,*,#20026,.F.) ;
#29172=ORIENTED_EDGE('',*,*,#20022,.T.) ;
#29173=ORIENTED_EDGE('',*,*,#20024,.T.) ;
#29174=ORIENTED_EDGE('',*,*,#20010,.F.) ;
#29175=ORIENTED_EDGE('',*,*,#20025,.F.) ;
#29176=ORIENTED_EDGE('',*,*,#20027,.F.) ;
#29177=ORIENTED_EDGE('',*,*,#20028,.F.) ;
#29178=ORIENTED_EDGE('',*,*,#20029,.F.) ;
#29179=ORIENTED_EDGE('',*,*,#20030,.F.) ;
#29180=ORIENTED_EDGE('',*,*,#20031,.T.) ;
#29181=ORIENTED_EDGE('',*,*,#20032,.F.) ;
#29182=ORIENTED_EDGE('',*,*,#20033,.T.) ;
#29183=ORIENTED_EDGE('',*,*,#20034,.T.) ;
#29184=ORIENTED_EDGE('',*,*,#20035,.F.) ;
#29185=ORIENTED_EDGE('',*,*,#20036,.T.) ;
#29186=ORIENTED_EDGE('',*,*,#20037,.T.) ;
#29187=ORIENTED_EDGE('',*,*,#20038,.T.) ;
#29188=ORIENTED_EDGE('',*,*,#20039,.T.) ;
#29189=ORIENTED_EDGE('',*,*,#20035,.T.) ;
#29190=ORIENTED_EDGE('',*,*,#20040,.T.) ;
#29191=ORIENTED_EDGE('',*,*,#20029,.T.) ;
#29192=ORIENTED_EDGE('',*,*,#20041,.T.) ;
#29193=ORIENTED_EDGE('',*,*,#20031,.F.) ;
#29194=ORIENTED_EDGE('',*,*,#20042,.T.) ;
#29195=ORIENTED_EDGE('',*,*,#20027,.T.) ;
#29196=ORIENTED_EDGE('',*,*,#20043,.F.) ;
#29197=ORIENTED_EDGE('',*,*,#20034,.F.) ;
#29198=ORIENTED_EDGE('',*,*,#20043,.T.) ;
#29199=ORIENTED_EDGE('',*,*,#20030,.T.) ;
#29200=ORIENTED_EDGE('',*,*,#20040,.F.) ;
#29201=ORIENTED_EDGE('',*,*,#20038,.F.) ;
#29202=ORIENTED_EDGE('',*,*,#20044,.F.) ;
#29203=ORIENTED_EDGE('',*,*,#20045,.F.) ;
#29204=ORIENTED_EDGE('',*,*,#20046,.F.) ;
#29205=ORIENTED_EDGE('',*,*,#20047,.F.) ;
#29206=ORIENTED_EDGE('',*,*,#20048,.T.) ;
#29207=ORIENTED_EDGE('',*,*,#20049,.F.) ;
#29208=ORIENTED_EDGE('',*,*,#20050,.T.) ;
#29209=ORIENTED_EDGE('',*,*,#20051,.T.) ;
#29210=ORIENTED_EDGE('',*,*,#20052,.F.) ;
#29211=ORIENTED_EDGE('',*,*,#20053,.T.) ;
#29212=ORIENTED_EDGE('',*,*,#20054,.T.) ;
#29213=ORIENTED_EDGE('',*,*,#20055,.T.) ;
#29214=ORIENTED_EDGE('',*,*,#20056,.T.) ;
#29215=ORIENTED_EDGE('',*,*,#20052,.T.) ;
#29216=ORIENTED_EDGE('',*,*,#20057,.T.) ;
#29217=ORIENTED_EDGE('',*,*,#20046,.T.) ;
#29218=ORIENTED_EDGE('',*,*,#20058,.T.) ;
#29219=ORIENTED_EDGE('',*,*,#20048,.F.) ;
#29220=ORIENTED_EDGE('',*,*,#20059,.T.) ;
#29221=ORIENTED_EDGE('',*,*,#20044,.T.) ;
#29222=ORIENTED_EDGE('',*,*,#20060,.F.) ;
#29223=ORIENTED_EDGE('',*,*,#20051,.F.) ;
#29224=ORIENTED_EDGE('',*,*,#20060,.T.) ;
#29225=ORIENTED_EDGE('',*,*,#20047,.T.) ;
#29226=ORIENTED_EDGE('',*,*,#20057,.F.) ;
#29227=ORIENTED_EDGE('',*,*,#20055,.F.) ;
#29228=ORIENTED_EDGE('',*,*,#20061,.T.) ;
#29229=ORIENTED_EDGE('',*,*,#19869,.T.) ;
#29230=ORIENTED_EDGE('',*,*,#19904,.T.) ;
#29231=ORIENTED_EDGE('',*,*,#19932,.T.) ;
#29232=ORIENTED_EDGE('',*,*,#19978,.T.) ;
#29233=ORIENTED_EDGE('',*,*,#19985,.T.) ;
#29234=ORIENTED_EDGE('',*,*,#19906,.T.) ;
#29235=ORIENTED_EDGE('',*,*,#19986,.T.) ;
#29236=ORIENTED_EDGE('',*,*,#19982,.F.) ;
#29237=ORIENTED_EDGE('',*,*,#19933,.T.) ;
#29238=ORIENTED_EDGE('',*,*,#19900,.T.) ;
#29239=ORIENTED_EDGE('',*,*,#19878,.T.) ;
#29240=ORIENTED_EDGE('',*,*,#20062,.T.) ;
#29241=ORIENTED_EDGE('',*,*,#20063,.F.) ;
#29242=ORIENTED_EDGE('',*,*,#20064,.F.) ;
#29243=ORIENTED_EDGE('',*,*,#20000,.T.) ;
#29244=ORIENTED_EDGE('',*,*,#20009,.T.) ;
#29245=ORIENTED_EDGE('',*,*,#19995,.F.) ;
#29246=ORIENTED_EDGE('',*,*,#20006,.T.) ;
#29247=ORIENTED_EDGE('',*,*,#19998,.F.) ;
#29248=ORIENTED_EDGE('',*,*,#20065,.F.) ;
#29249=ORIENTED_EDGE('',*,*,#20066,.F.) ;
#29250=ORIENTED_EDGE('',*,*,#20067,.T.) ;
#29251=ORIENTED_EDGE('',*,*,#19872,.T.) ;
#29252=ORIENTED_EDGE('',*,*,#19894,.T.) ;
#29253=ORIENTED_EDGE('',*,*,#19991,.T.) ;
#29254=ORIENTED_EDGE('',*,*,#19955,.T.) ;
#29255=ORIENTED_EDGE('',*,*,#19964,.T.) ;
#29256=ORIENTED_EDGE('',*,*,#19909,.T.) ;
#29257=ORIENTED_EDGE('',*,*,#19965,.T.) ;
#29258=ORIENTED_EDGE('',*,*,#19957,.F.) ;
#29259=ORIENTED_EDGE('',*,*,#19992,.T.) ;
#29260=ORIENTED_EDGE('',*,*,#19890,.T.) ;
#29261=ORIENTED_EDGE('',*,*,#19874,.T.) ;
#29262=ORIENTED_EDGE('',*,*,#20068,.T.) ;
#29263=ORIENTED_EDGE('',*,*,#20069,.F.) ;
#29264=ORIENTED_EDGE('',*,*,#20070,.F.) ;
#29265=ORIENTED_EDGE('',*,*,#20049,.T.) ;
#29266=ORIENTED_EDGE('',*,*,#20058,.F.) ;
#29267=ORIENTED_EDGE('',*,*,#20045,.T.) ;
#29268=ORIENTED_EDGE('',*,*,#20059,.F.) ;
#29269=ORIENTED_EDGE('',*,*,#20054,.F.) ;
#29270=ORIENTED_EDGE('',*,*,#20071,.F.) ;
#29271=ORIENTED_EDGE('',*,*,#20072,.F.) ;
#29272=ORIENTED_EDGE('',*,*,#20073,.T.) ;
#29273=ORIENTED_EDGE('',*,*,#19876,.T.) ;
#29274=ORIENTED_EDGE('',*,*,#19889,.T.) ;
#29275=ORIENTED_EDGE('',*,*,#19939,.T.) ;
#29276=ORIENTED_EDGE('',*,*,#19943,.T.) ;
#29277=ORIENTED_EDGE('',*,*,#19950,.T.) ;
#29278=ORIENTED_EDGE('',*,*,#19914,.T.) ;
#29279=ORIENTED_EDGE('',*,*,#19951,.T.) ;
#29280=ORIENTED_EDGE('',*,*,#19947,.F.) ;
#29281=ORIENTED_EDGE('',*,*,#19940,.T.) ;
#29282=ORIENTED_EDGE('',*,*,#19885,.T.) ;
#29283=ORIENTED_EDGE('',*,*,#19867,.T.) ;
#29284=ORIENTED_EDGE('',*,*,#20074,.T.) ;
#29285=ORIENTED_EDGE('',*,*,#20075,.F.) ;
#29286=ORIENTED_EDGE('',*,*,#20076,.F.) ;
#29287=ORIENTED_EDGE('',*,*,#20017,.T.) ;
#29288=ORIENTED_EDGE('',*,*,#20026,.T.) ;
#29289=ORIENTED_EDGE('',*,*,#20012,.F.) ;
#29290=ORIENTED_EDGE('',*,*,#20023,.T.) ;
#29291=ORIENTED_EDGE('',*,*,#20015,.F.) ;
#29292=ORIENTED_EDGE('',*,*,#20077,.F.) ;
#29293=ORIENTED_EDGE('',*,*,#20078,.F.) ;
#29294=ORIENTED_EDGE('',*,*,#20079,.T.) ;
#29295=ORIENTED_EDGE('',*,*,#19880,.T.) ;
#29296=ORIENTED_EDGE('',*,*,#19899,.T.) ;
#29297=ORIENTED_EDGE('',*,*,#19925,.T.) ;
#29298=ORIENTED_EDGE('',*,*,#19967,.T.) ;
#29299=ORIENTED_EDGE('',*,*,#19975,.T.) ;
#29300=ORIENTED_EDGE('',*,*,#19917,.T.) ;
#29301=ORIENTED_EDGE('',*,*,#19976,.T.) ;
#29302=ORIENTED_EDGE('',*,*,#19971,.F.) ;
#29303=ORIENTED_EDGE('',*,*,#19926,.T.) ;
#29304=ORIENTED_EDGE('',*,*,#19895,.T.) ;
#29305=ORIENTED_EDGE('',*,*,#19863,.T.) ;
#29306=ORIENTED_EDGE('',*,*,#20080,.T.) ;
#29307=ORIENTED_EDGE('',*,*,#20081,.F.) ;
#29308=ORIENTED_EDGE('',*,*,#20082,.F.) ;
#29309=ORIENTED_EDGE('',*,*,#20032,.T.) ;
#29310=ORIENTED_EDGE('',*,*,#20041,.F.) ;
#29311=ORIENTED_EDGE('',*,*,#20028,.T.) ;
#29312=ORIENTED_EDGE('',*,*,#20042,.F.) ;
#29313=ORIENTED_EDGE('',*,*,#20037,.F.) ;
#29314=ORIENTED_EDGE('',*,*,#20083,.F.) ;
#29315=ORIENTED_EDGE('',*,*,#20084,.F.) ;
#29316=ORIENTED_EDGE('',*,*,#20065,.T.) ;
#29317=ORIENTED_EDGE('',*,*,#19997,.F.) ;
#29318=ORIENTED_EDGE('',*,*,#20004,.F.) ;
#29319=ORIENTED_EDGE('',*,*,#20001,.F.) ;
#29320=ORIENTED_EDGE('',*,*,#20064,.T.) ;
#29321=ORIENTED_EDGE('',*,*,#20085,.F.) ;
#29322=ORIENTED_EDGE('',*,*,#20083,.T.) ;
#29323=ORIENTED_EDGE('',*,*,#20036,.F.) ;
#29324=ORIENTED_EDGE('',*,*,#20039,.F.) ;
#29325=ORIENTED_EDGE('',*,*,#20033,.F.) ;
#29326=ORIENTED_EDGE('',*,*,#20082,.T.) ;
#29327=ORIENTED_EDGE('',*,*,#20086,.F.) ;
#29328=ORIENTED_EDGE('',*,*,#20087,.F.) ;
#29329=ORIENTED_EDGE('',*,*,#20071,.T.) ;
#29330=ORIENTED_EDGE('',*,*,#20053,.F.) ;
#29331=ORIENTED_EDGE('',*,*,#20056,.F.) ;
#29332=ORIENTED_EDGE('',*,*,#20050,.F.) ;
#29333=ORIENTED_EDGE('',*,*,#20070,.T.) ;
#29334=ORIENTED_EDGE('',*,*,#20088,.F.) ;
#29335=ORIENTED_EDGE('',*,*,#20077,.T.) ;
#29336=ORIENTED_EDGE('',*,*,#20014,.F.) ;
#29337=ORIENTED_EDGE('',*,*,#20021,.F.) ;
#29338=ORIENTED_EDGE('',*,*,#20018,.F.) ;
#29339=ORIENTED_EDGE('',*,*,#20076,.T.) ;
#29340=ORIENTED_EDGE('',*,*,#20089,.F.) ;
#29341=ORIENTED_EDGE('',*,*,#19884,.F.) ;
#29342=ORIENTED_EDGE('',*,*,#20090,.T.) ;
#29343=ORIENTED_EDGE('',*,*,#20091,.T.) ;
#29344=ORIENTED_EDGE('',*,*,#20089,.T.) ;
#29345=ORIENTED_EDGE('',*,*,#20092,.T.) ;
#29346=ORIENTED_EDGE('',*,*,#20093,.T.) ;
#29347=ORIENTED_EDGE('',*,*,#20066,.T.) ;
#29348=ORIENTED_EDGE('',*,*,#20091,.F.) ;
#29349=ORIENTED_EDGE('',*,*,#20094,.T.) ;
#29350=ORIENTED_EDGE('',*,*,#20092,.F.) ;
#29351=ORIENTED_EDGE('',*,*,#20075,.T.) ;
#29352=ORIENTED_EDGE('',*,*,#20095,.T.) ;
#29353=ORIENTED_EDGE('',*,*,#20096,.T.) ;
#29354=ORIENTED_EDGE('',*,*,#20088,.T.) ;
#29355=ORIENTED_EDGE('',*,*,#20097,.T.) ;
#29356=ORIENTED_EDGE('',*,*,#20098,.T.) ;
#29357=ORIENTED_EDGE('',*,*,#20097,.F.) ;
#29358=ORIENTED_EDGE('',*,*,#20069,.T.) ;
#29359=ORIENTED_EDGE('',*,*,#20099,.T.) ;
#29360=ORIENTED_EDGE('',*,*,#20078,.T.) ;
#29361=ORIENTED_EDGE('',*,*,#20096,.F.) ;
#29362=ORIENTED_EDGE('',*,*,#20100,.T.) ;
#29363=ORIENTED_EDGE('',*,*,#20101,.T.) ;
#29364=ORIENTED_EDGE('',*,*,#20087,.T.) ;
#29365=ORIENTED_EDGE('',*,*,#20102,.F.) ;
#29366=ORIENTED_EDGE('',*,*,#20103,.T.) ;
#29367=ORIENTED_EDGE('',*,*,#20102,.T.) ;
#29368=ORIENTED_EDGE('',*,*,#20086,.T.) ;
#29369=ORIENTED_EDGE('',*,*,#20104,.T.) ;
#29370=ORIENTED_EDGE('',*,*,#20105,.T.) ;
#29371=ORIENTED_EDGE('',*,*,#20072,.T.) ;
#29372=ORIENTED_EDGE('',*,*,#20101,.F.) ;
#29373=ORIENTED_EDGE('',*,*,#20106,.T.) ;
#29374=ORIENTED_EDGE('',*,*,#20104,.F.) ;
#29375=ORIENTED_EDGE('',*,*,#20081,.T.) ;
#29376=ORIENTED_EDGE('',*,*,#20107,.T.) ;
#29377=ORIENTED_EDGE('',*,*,#20108,.T.) ;
#29378=ORIENTED_EDGE('',*,*,#20085,.T.) ;
#29379=ORIENTED_EDGE('',*,*,#20109,.T.) ;
#29380=ORIENTED_EDGE('',*,*,#20110,.T.) ;
#29381=ORIENTED_EDGE('',*,*,#20109,.F.) ;
#29382=ORIENTED_EDGE('',*,*,#20063,.T.) ;
#29383=ORIENTED_EDGE('',*,*,#20111,.T.) ;
#29384=ORIENTED_EDGE('',*,*,#20084,.T.) ;
#29385=ORIENTED_EDGE('',*,*,#20108,.F.) ;
#29386=ORIENTED_EDGE('',*,*,#20100,.F.) ;
#29387=ORIENTED_EDGE('',*,*,#20103,.F.) ;
#29388=ORIENTED_EDGE('',*,*,#20106,.F.) ;
#29389=ORIENTED_EDGE('',*,*,#20080,.F.) ;
#29390=ORIENTED_EDGE('',*,*,#19866,.T.) ;
#29391=ORIENTED_EDGE('',*,*,#19873,.T.) ;
#29392=ORIENTED_EDGE('',*,*,#20067,.F.) ;
#29393=ORIENTED_EDGE('',*,*,#20105,.F.) ;
#29394=ORIENTED_EDGE('',*,*,#20074,.F.) ;
#29395=ORIENTED_EDGE('',*,*,#19870,.T.) ;
#29396=ORIENTED_EDGE('',*,*,#20061,.F.) ;
#29397=ORIENTED_EDGE('',*,*,#20093,.F.) ;
#29398=ORIENTED_EDGE('',*,*,#20090,.F.) ;
#29399=ORIENTED_EDGE('',*,*,#20094,.F.) ;
#29400=ORIENTED_EDGE('',*,*,#20095,.F.) ;
#29401=ORIENTED_EDGE('',*,*,#20098,.F.) ;
#29402=ORIENTED_EDGE('',*,*,#20068,.F.) ;
#29403=ORIENTED_EDGE('',*,*,#19877,.T.) ;
#29404=ORIENTED_EDGE('',*,*,#20073,.F.) ;
#29405=ORIENTED_EDGE('',*,*,#20099,.F.) ;
#29406=ORIENTED_EDGE('',*,*,#20107,.F.) ;
#29407=ORIENTED_EDGE('',*,*,#20110,.F.) ;
#29408=ORIENTED_EDGE('',*,*,#20062,.F.) ;
#29409=ORIENTED_EDGE('',*,*,#19881,.T.) ;
#29410=ORIENTED_EDGE('',*,*,#20079,.F.) ;
#29411=ORIENTED_EDGE('',*,*,#20111,.F.) ;
#30670=CYLINDRICAL_SURFACE('',#36155,1.651) ;
#30671=CYLINDRICAL_SURFACE('',#36175,0.095249999999997) ;
#30672=CYLINDRICAL_SURFACE('',#36177,0.0952499999999953) ;
#30673=CYLINDRICAL_SURFACE('',#36183,0.095249999999997) ;
#30674=CYLINDRICAL_SURFACE('',#36185,0.0952499999999975) ;
#30675=CYLINDRICAL_SURFACE('',#36191,0.0952500000000012) ;
#30676=CYLINDRICAL_SURFACE('',#36193,0.0952500000000014) ;
#30677=CYLINDRICAL_SURFACE('',#36197,0.635) ;
#30678=CYLINDRICAL_SURFACE('',#36199,0.0635000000000001) ;
#30679=CYLINDRICAL_SURFACE('',#36202,0.0635000000000013) ;
#30680=CYLINDRICAL_SURFACE('',#36212,0.0634999999999983) ;
#30681=CYLINDRICAL_SURFACE('',#36214,0.0635000000000001) ;
#30682=CYLINDRICAL_SURFACE('',#36218,0.635) ;
#30683=CYLINDRICAL_SURFACE('',#36223,0.0634999999999983) ;
#30684=CYLINDRICAL_SURFACE('',#36225,0.0635000000000001) ;
#30685=CYLINDRICAL_SURFACE('',#36229,0.635) ;
#30686=CYLINDRICAL_SURFACE('',#36231,0.0635000000000001) ;
#30687=CYLINDRICAL_SURFACE('',#36234,0.0635000000000012) ;
#30688=CYLINDRICAL_SURFACE('',#36238,0.635) ;
#30689=CYLINDRICAL_SURFACE('',#36243,0.0952500000000027) ;
#30690=CYLINDRICAL_SURFACE('',#36245,0.0952499999999953) ;
#30691=CYLINDRICAL_SURFACE('',#36251,0.635000000000001) ;
#30692=CYLINDRICAL_SURFACE('',#36254,0.189865) ;
#30693=CYLINDRICAL_SURFACE('',#36257,0.189865) ;
#30694=CYLINDRICAL_SURFACE('',#36265,0.635000000000001) ;
#30695=CYLINDRICAL_SURFACE('',#36268,0.189865) ;
#30696=CYLINDRICAL_SURFACE('',#36271,0.189865) ;
#30697=CYLINDRICAL_SURFACE('',#36279,0.635) ;
#30698=CYLINDRICAL_SURFACE('',#36282,0.189865000000002) ;
#30699=CYLINDRICAL_SURFACE('',#36285,0.189865000000002) ;
#30700=CYLINDRICAL_SURFACE('',#36293,0.635) ;
#30701=CYLINDRICAL_SURFACE('',#36296,0.189865000000002) ;
#30702=CYLINDRICAL_SURFACE('',#36299,0.189865000000002) ;
#30703=CYLINDRICAL_SURFACE('',#36326,5.22940367264148) ;
#30704=CYLINDRICAL_SURFACE('',#36327,5.22940367264148) ;
#30705=CYLINDRICAL_SURFACE('',#36328,5.22940367264148) ;
#30706=CYLINDRICAL_SURFACE('',#36329,5.22940367264148) ;
#32440=ADVANCED_FACE('',(#3961),#748,.T.) ;
#32441=ADVANCED_FACE('',(#3962),#749,.T.) ;
#32442=ADVANCED_FACE('',(#3963),#750,.T.) ;
#32443=ADVANCED_FACE('',(#3964),#751,.T.) ;
#32444=ADVANCED_FACE('',(#3965),#752,.T.) ;
#32445=ADVANCED_FACE('',(#3966),#30670,.F.) ;
#32446=ADVANCED_FACE('',(#3967,#1173),#2191,.T.) ;
#32447=ADVANCED_FACE('',(#3968),#2192,.T.) ;
#32448=ADVANCED_FACE('',(#3969),#2193,.T.) ;
#32449=ADVANCED_FACE('',(#3970),#2194,.T.) ;
#32450=ADVANCED_FACE('',(#3971),#2195,.T.) ;
#32451=ADVANCED_FACE('',(#3972),#456,.T.) ;
#32452=ADVANCED_FACE('',(#3973),#30671,.T.) ;
#32453=ADVANCED_FACE('',(#3974),#30672,.T.) ;
#32454=ADVANCED_FACE('',(#3975),#457,.T.) ;
#32455=ADVANCED_FACE('',(#3976),#30673,.T.) ;
#32456=ADVANCED_FACE('',(#3977),#30674,.T.) ;
#32457=ADVANCED_FACE('',(#3978),#458,.T.) ;
#32458=ADVANCED_FACE('',(#3979),#30675,.T.) ;
#32459=ADVANCED_FACE('',(#3980),#30676,.T.) ;
#32460=ADVANCED_FACE('',(#3981),#2196,.T.) ;
#32461=ADVANCED_FACE('',(#3982),#2197,.T.) ;
#32462=ADVANCED_FACE('',(#3983),#30677,.F.) ;
#32463=ADVANCED_FACE('',(#3984),#30678,.F.) ;
#32464=ADVANCED_FACE('',(#3985),#30679,.F.) ;
#32465=ADVANCED_FACE('',(#3986),#459,.F.) ;
#32466=ADVANCED_FACE('',(#3987),#2198,.T.) ;
#32467=ADVANCED_FACE('',(#3988),#2199,.T.) ;
#32468=ADVANCED_FACE('',(#3989),#460,.F.) ;
#32469=ADVANCED_FACE('',(#3990),#30680,.F.) ;
#32470=ADVANCED_FACE('',(#3991),#30681,.F.) ;
#32471=ADVANCED_FACE('',(#3992),#2200,.T.) ;
#32472=ADVANCED_FACE('',(#3993),#2201,.T.) ;
#32473=ADVANCED_FACE('',(#3994),#30682,.F.) ;
#32474=ADVANCED_FACE('',(#3995),#461,.F.) ;
#32475=ADVANCED_FACE('',(#3996),#30683,.F.) ;
#32476=ADVANCED_FACE('',(#3997),#30684,.F.) ;
#32477=ADVANCED_FACE('',(#3998),#2202,.T.) ;
#32478=ADVANCED_FACE('',(#3999),#2203,.T.) ;
#32479=ADVANCED_FACE('',(#4000),#30685,.F.) ;
#32480=ADVANCED_FACE('',(#4001),#30686,.F.) ;
#32481=ADVANCED_FACE('',(#4002),#30687,.F.) ;
#32482=ADVANCED_FACE('',(#4003),#462,.F.) ;
#32483=ADVANCED_FACE('',(#4004),#30688,.F.) ;
#32484=ADVANCED_FACE('',(#4005),#463,.T.) ;
#32485=ADVANCED_FACE('',(#4006),#30689,.T.) ;
#32486=ADVANCED_FACE('',(#4007),#30690,.T.) ;
#32487=ADVANCED_FACE('',(#4008),#2204,.T.) ;
#32488=ADVANCED_FACE('',(#4009),#2205,.T.) ;
#32489=ADVANCED_FACE('',(#4010),#2206,.T.) ;
#32490=ADVANCED_FACE('',(#4011),#30691,.T.) ;
#32491=ADVANCED_FACE('',(#4012),#30692,.T.) ;
#32492=ADVANCED_FACE('',(#4013),#30693,.T.) ;
#32493=ADVANCED_FACE('',(#4014),#464,.T.) ;
#32494=ADVANCED_FACE('',(#4015),#2207,.T.) ;
#32495=ADVANCED_FACE('',(#4016),#2208,.T.) ;
#32496=ADVANCED_FACE('',(#4017),#2209,.T.) ;
#32497=ADVANCED_FACE('',(#4018),#30694,.T.) ;
#32498=ADVANCED_FACE('',(#4019),#30695,.T.) ;
#32499=ADVANCED_FACE('',(#4020),#30696,.T.) ;
#32500=ADVANCED_FACE('',(#4021),#465,.T.) ;
#32501=ADVANCED_FACE('',(#4022),#2210,.T.) ;
#32502=ADVANCED_FACE('',(#4023),#2211,.T.) ;
#32503=ADVANCED_FACE('',(#4024),#2212,.T.) ;
#32504=ADVANCED_FACE('',(#4025),#30697,.T.) ;
#32505=ADVANCED_FACE('',(#4026),#30698,.T.) ;
#32506=ADVANCED_FACE('',(#4027),#30699,.T.) ;
#32507=ADVANCED_FACE('',(#4028),#466,.T.) ;
#32508=ADVANCED_FACE('',(#4029),#2213,.T.) ;
#32509=ADVANCED_FACE('',(#4030),#2214,.T.) ;
#32510=ADVANCED_FACE('',(#4031),#2215,.T.) ;
#32511=ADVANCED_FACE('',(#4032),#30700,.T.) ;
#32512=ADVANCED_FACE('',(#4033),#30701,.T.) ;
#32513=ADVANCED_FACE('',(#4034),#30702,.T.) ;
#32514=ADVANCED_FACE('',(#4035),#467,.T.) ;
#32515=ADVANCED_FACE('',(#4036),#2216,.T.) ;
#32516=ADVANCED_FACE('',(#4037),#2217,.T.) ;
#32517=ADVANCED_FACE('',(#4038),#2218,.T.) ;
#32518=ADVANCED_FACE('',(#4039),#2219,.T.) ;
#32519=ADVANCED_FACE('',(#4040,#1174),#2220,.T.) ;
#32520=ADVANCED_FACE('',(#4041),#753,.T.) ;
#32521=ADVANCED_FACE('',(#4042),#2221,.T.) ;
#32522=ADVANCED_FACE('',(#4043),#2222,.T.) ;
#32523=ADVANCED_FACE('',(#4044),#754,.T.) ;
#32524=ADVANCED_FACE('',(#4045),#2223,.T.) ;
#32525=ADVANCED_FACE('',(#4046),#2224,.T.) ;
#32526=ADVANCED_FACE('',(#4047),#755,.T.) ;
#32527=ADVANCED_FACE('',(#4048),#756,.T.) ;
#32528=ADVANCED_FACE('',(#4049),#2225,.T.) ;
#32529=ADVANCED_FACE('',(#4050),#2226,.T.) ;
#32530=ADVANCED_FACE('',(#4051),#757,.T.) ;
#32531=ADVANCED_FACE('',(#4052),#2227,.T.) ;
#32532=ADVANCED_FACE('',(#4053),#2228,.T.) ;
#32533=ADVANCED_FACE('',(#4054),#30703,.T.) ;
#32534=ADVANCED_FACE('',(#4055),#30704,.T.) ;
#32535=ADVANCED_FACE('',(#4056),#30705,.T.) ;
#32536=ADVANCED_FACE('',(#4057),#30706,.T.) ;
#32644=CLOSED_SHELL('',(#32440,#32441,#32442,#32443,#32444,#32445,#32446,
#32447,#32448,#32449,#32450,#32451,#32452,#32453,#32454,#32455,#32456,#32457,
#32458,#32459,#32460,#32461,#32462,#32463,#32464,#32465,#32466,#32467,#32468,
#32469,#32470,#32471,#32472,#32473,#32474,#32475,#32476,#32477,#32478,#32479,
#32480,#32481,#32482,#32483,#32484,#32485,#32486,#32487,#32488,#32489,#32490,
#32491,#32492,#32493,#32494,#32495,#32496,#32497,#32498,#32499,#32500,#32501,
#32502,#32503,#32504,#32505,#32506,#32507,#32508,#32509,#32510,#32511,#32512,
#32513,#32514,#32515,#32516,#32517,#32518,#32519,#32520,#32521,#32522,#32523,
#32524,#32525,#32526,#32527,#32528,#32529,#32530,#32531,#32532,#32533,#32534,
#32535,#32536)) ;
#36144=AXIS2_PLACEMENT_3D('',#80803,#45330,#45331) ;
#36145=AXIS2_PLACEMENT_3D('',#80840,#45332,#45333) ;
#36146=AXIS2_PLACEMENT_3D('',#80846,#45334,#45335) ;
#36147=AXIS2_PLACEMENT_3D('',#80883,#45336,#45337) ;
#36148=AXIS2_PLACEMENT_3D('',#80891,#45338,#45339) ;
#36149=AXIS2_PLACEMENT_3D('',#80920,#45340,#45341) ;
#36150=AXIS2_PLACEMENT_3D('',#80928,#45342,#45343) ;
#36151=AXIS2_PLACEMENT_3D('',#80965,#45344,#45345) ;
#36152=AXIS2_PLACEMENT_3D('',#80973,#45346,#45347) ;
#36153=AXIS2_PLACEMENT_3D('',#81010,#45348,#45349) ;
#36154=AXIS2_PLACEMENT_3D('',#81018,#45350,#45351) ;
#36155=AXIS2_PLACEMENT_3D('',#81019,#45352,#45353) ;
#36156=AXIS2_PLACEMENT_3D('',#81021,#45354,#45355) ;
#36157=AXIS2_PLACEMENT_3D('',#81024,#45357,#45358) ;
#36158=AXIS2_PLACEMENT_3D('',#81025,#45359,#45360) ;
#36159=AXIS2_PLACEMENT_3D('',#81031,#45363,#45364) ;
#36160=AXIS2_PLACEMENT_3D('',#81040,#45369,#45370) ;
#36161=AXIS2_PLACEMENT_3D('',#81049,#45375,#45376) ;
#36162=AXIS2_PLACEMENT_3D('',#81058,#45381,#45382) ;
#36163=AXIS2_PLACEMENT_3D('',#81062,#45385,#45386) ;
#36164=AXIS2_PLACEMENT_3D('',#81070,#45390,#45391) ;
#36165=AXIS2_PLACEMENT_3D('',#81071,#45392,#45393) ;
#36166=AXIS2_PLACEMENT_3D('',#81078,#45396,#45397) ;
#36167=AXIS2_PLACEMENT_3D('',#81080,#45399,#45400) ;
#36168=AXIS2_PLACEMENT_3D('',#81088,#45404,#45405) ;
#36169=AXIS2_PLACEMENT_3D('',#81089,#45406,#45407) ;
#36170=AXIS2_PLACEMENT_3D('',#81096,#45410,#45411) ;
#36171=AXIS2_PLACEMENT_3D('',#81098,#45413,#45414) ;
#36172=AXIS2_PLACEMENT_3D('',#81100,#45415,#45416) ;
#36173=AXIS2_PLACEMENT_3D('',#81102,#45417,#45418) ;
#36174=AXIS2_PLACEMENT_3D('',#81103,#45419,#45420) ;
#36175=AXIS2_PLACEMENT_3D('',#81104,#45421,#45422) ;
#36176=AXIS2_PLACEMENT_3D('',#81107,#45424,#45425) ;
#36177=AXIS2_PLACEMENT_3D('',#81108,#45426,#45427) ;
#36178=AXIS2_PLACEMENT_3D('',#81110,#45428,#45429) ;
#36179=AXIS2_PLACEMENT_3D('',#81112,#45431,#45432) ;
#36180=AXIS2_PLACEMENT_3D('',#81114,#45433,#45434) ;
#36181=AXIS2_PLACEMENT_3D('',#81116,#45435,#45436) ;
#36182=AXIS2_PLACEMENT_3D('',#81117,#45437,#45438) ;
#36183=AXIS2_PLACEMENT_3D('',#81118,#45439,#45440) ;
#36184=AXIS2_PLACEMENT_3D('',#81121,#45442,#45443) ;
#36185=AXIS2_PLACEMENT_3D('',#81122,#45444,#45445) ;
#36186=AXIS2_PLACEMENT_3D('',#81124,#45446,#45447) ;
#36187=AXIS2_PLACEMENT_3D('',#81126,#45449,#45450) ;
#36188=AXIS2_PLACEMENT_3D('',#81128,#45451,#45452) ;
#36189=AXIS2_PLACEMENT_3D('',#81130,#45453,#45454) ;
#36190=AXIS2_PLACEMENT_3D('',#81131,#45455,#45456) ;
#36191=AXIS2_PLACEMENT_3D('',#81132,#45457,#45458) ;
#36192=AXIS2_PLACEMENT_3D('',#81135,#45460,#45461) ;
#36193=AXIS2_PLACEMENT_3D('',#81136,#45462,#45463) ;
#36194=AXIS2_PLACEMENT_3D('',#81138,#45464,#45465) ;
#36195=AXIS2_PLACEMENT_3D('',#81140,#45467,#45468) ;
#36196=AXIS2_PLACEMENT_3D('',#81146,#45472,#45473) ;
#36197=AXIS2_PLACEMENT_3D('',#81152,#45477,#45478) ;
#36198=AXIS2_PLACEMENT_3D('',#81153,#45479,#45480) ;
#36199=AXIS2_PLACEMENT_3D('',#81154,#45481,#45482) ;
#36200=AXIS2_PLACEMENT_3D('',#81155,#45483,#45484) ;
#36201=AXIS2_PLACEMENT_3D('',#81156,#45485,#45486) ;
#36202=AXIS2_PLACEMENT_3D('',#81157,#45487,#45488) ;
#36203=AXIS2_PLACEMENT_3D('',#81158,#45489,#45490) ;
#36204=AXIS2_PLACEMENT_3D('',#81159,#45491,#45492) ;
#36205=AXIS2_PLACEMENT_3D('',#81160,#45493,#45494) ;
#36206=AXIS2_PLACEMENT_3D('',#81161,#45495,#45496) ;
#36207=AXIS2_PLACEMENT_3D('',#81170,#45501,#45502) ;
#36208=AXIS2_PLACEMENT_3D('',#81179,#45507,#45508) ;
#36209=AXIS2_PLACEMENT_3D('',#81180,#45509,#45510) ;
#36210=AXIS2_PLACEMENT_3D('',#81181,#45511,#45512) ;
#36211=AXIS2_PLACEMENT_3D('',#81182,#45513,#45514) ;
#36212=AXIS2_PLACEMENT_3D('',#81183,#45515,#45516) ;
#36213=AXIS2_PLACEMENT_3D('',#81184,#45517,#45518) ;
#36214=AXIS2_PLACEMENT_3D('',#81185,#45519,#45520) ;
#36215=AXIS2_PLACEMENT_3D('',#81186,#45521,#45522) ;
#36216=AXIS2_PLACEMENT_3D('',#81187,#45523,#45524) ;
#36217=AXIS2_PLACEMENT_3D('',#81193,#45528,#45529) ;
#36218=AXIS2_PLACEMENT_3D('',#81199,#45533,#45534) ;
#36219=AXIS2_PLACEMENT_3D('',#81200,#45535,#45536) ;
#36220=AXIS2_PLACEMENT_3D('',#81201,#45537,#45538) ;
#36221=AXIS2_PLACEMENT_3D('',#81202,#45539,#45540) ;
#36222=AXIS2_PLACEMENT_3D('',#81203,#45541,#45542) ;
#36223=AXIS2_PLACEMENT_3D('',#81204,#45543,#45544) ;
#36224=AXIS2_PLACEMENT_3D('',#81205,#45545,#45546) ;
#36225=AXIS2_PLACEMENT_3D('',#81206,#45547,#45548) ;
#36226=AXIS2_PLACEMENT_3D('',#81207,#45549,#45550) ;
#36227=AXIS2_PLACEMENT_3D('',#81208,#45551,#45552) ;
#36228=AXIS2_PLACEMENT_3D('',#81214,#45556,#45557) ;
#36229=AXIS2_PLACEMENT_3D('',#81220,#45561,#45562) ;
#36230=AXIS2_PLACEMENT_3D('',#81221,#45563,#45564) ;
#36231=AXIS2_PLACEMENT_3D('',#81222,#45565,#45566) ;
#36232=AXIS2_PLACEMENT_3D('',#81223,#45567,#45568) ;
#36233=AXIS2_PLACEMENT_3D('',#81224,#45569,#45570) ;
#36234=AXIS2_PLACEMENT_3D('',#81225,#45571,#45572) ;
#36235=AXIS2_PLACEMENT_3D('',#81226,#45573,#45574) ;
#36236=AXIS2_PLACEMENT_3D('',#81227,#45575,#45576) ;
#36237=AXIS2_PLACEMENT_3D('',#81228,#45577,#45578) ;
#36238=AXIS2_PLACEMENT_3D('',#81229,#45579,#45580) ;
#36239=AXIS2_PLACEMENT_3D('',#81230,#45581,#45582) ;
#36240=AXIS2_PLACEMENT_3D('',#81231,#45583,#45584) ;
#36241=AXIS2_PLACEMENT_3D('',#81232,#45585,#45586) ;
#36242=AXIS2_PLACEMENT_3D('',#81233,#45587,#45588) ;
#36243=AXIS2_PLACEMENT_3D('',#81234,#45589,#45590) ;
#36244=AXIS2_PLACEMENT_3D('',#81235,#45591,#45592) ;
#36245=AXIS2_PLACEMENT_3D('',#81236,#45593,#45594) ;
#36246=AXIS2_PLACEMENT_3D('',#81237,#45595,#45596) ;
#36247=AXIS2_PLACEMENT_3D('',#81238,#45597,#45598) ;
#36248=AXIS2_PLACEMENT_3D('',#81241,#45599,#45600) ;
#36249=AXIS2_PLACEMENT_3D('',#81247,#45604,#45605) ;
#36250=AXIS2_PLACEMENT_3D('',#81254,#45609,#45610) ;
#36251=AXIS2_PLACEMENT_3D('',#81263,#45615,#45616) ;
#36252=AXIS2_PLACEMENT_3D('',#81264,#45617,#45618) ;
#36253=AXIS2_PLACEMENT_3D('',#81265,#45619,#45620) ;
#36254=AXIS2_PLACEMENT_3D('',#81266,#45621,#45622) ;
#36255=AXIS2_PLACEMENT_3D('',#81267,#45623,#45624) ;
#36256=AXIS2_PLACEMENT_3D('',#81268,#45625,#45626) ;
#36257=AXIS2_PLACEMENT_3D('',#81269,#45627,#45628) ;
#36258=AXIS2_PLACEMENT_3D('',#81270,#45629,#45630) ;
#36259=AXIS2_PLACEMENT_3D('',#81271,#45631,#45632) ;
#36260=AXIS2_PLACEMENT_3D('',#81272,#45633,#45634) ;
#36261=AXIS2_PLACEMENT_3D('',#81273,#45635,#45636) ;
#36262=AXIS2_PLACEMENT_3D('',#81276,#45637,#45638) ;
#36263=AXIS2_PLACEMENT_3D('',#81282,#45642,#45643) ;
#36264=AXIS2_PLACEMENT_3D('',#81289,#45647,#45648) ;
#36265=AXIS2_PLACEMENT_3D('',#81298,#45653,#45654) ;
#36266=AXIS2_PLACEMENT_3D('',#81299,#45655,#45656) ;
#36267=AXIS2_PLACEMENT_3D('',#81300,#45657,#45658) ;
#36268=AXIS2_PLACEMENT_3D('',#81301,#45659,#45660) ;
#36269=AXIS2_PLACEMENT_3D('',#81302,#45661,#45662) ;
#36270=AXIS2_PLACEMENT_3D('',#81303,#45663,#45664) ;
#36271=AXIS2_PLACEMENT_3D('',#81304,#45665,#45666) ;
#36272=AXIS2_PLACEMENT_3D('',#81305,#45667,#45668) ;
#36273=AXIS2_PLACEMENT_3D('',#81306,#45669,#45670) ;
#36274=AXIS2_PLACEMENT_3D('',#81307,#45671,#45672) ;
#36275=AXIS2_PLACEMENT_3D('',#81308,#45673,#45674) ;
#36276=AXIS2_PLACEMENT_3D('',#81316,#45678,#45679) ;
#36277=AXIS2_PLACEMENT_3D('',#81317,#45680,#45681) ;
#36278=AXIS2_PLACEMENT_3D('',#81324,#45685,#45686) ;
#36279=AXIS2_PLACEMENT_3D('',#81333,#45691,#45692) ;
#36280=AXIS2_PLACEMENT_3D('',#81334,#45693,#45694) ;
#36281=AXIS2_PLACEMENT_3D('',#81335,#45695,#45696) ;
#36282=AXIS2_PLACEMENT_3D('',#81336,#45697,#45698) ;
#36283=AXIS2_PLACEMENT_3D('',#81337,#45699,#45700) ;
#36284=AXIS2_PLACEMENT_3D('',#81338,#45701,#45702) ;
#36285=AXIS2_PLACEMENT_3D('',#81339,#45703,#45704) ;
#36286=AXIS2_PLACEMENT_3D('',#81340,#45705,#45706) ;
#36287=AXIS2_PLACEMENT_3D('',#81341,#45707,#45708) ;
#36288=AXIS2_PLACEMENT_3D('',#81342,#45709,#45710) ;
#36289=AXIS2_PLACEMENT_3D('',#81343,#45711,#45712) ;
#36290=AXIS2_PLACEMENT_3D('',#81351,#45716,#45717) ;
#36291=AXIS2_PLACEMENT_3D('',#81352,#45718,#45719) ;
#36292=AXIS2_PLACEMENT_3D('',#81359,#45723,#45724) ;
#36293=AXIS2_PLACEMENT_3D('',#81368,#45729,#45730) ;
#36294=AXIS2_PLACEMENT_3D('',#81369,#45731,#45732) ;
#36295=AXIS2_PLACEMENT_3D('',#81370,#45733,#45734) ;
#36296=AXIS2_PLACEMENT_3D('',#81371,#45735,#45736) ;
#36297=AXIS2_PLACEMENT_3D('',#81372,#45737,#45738) ;
#36298=AXIS2_PLACEMENT_3D('',#81373,#45739,#45740) ;
#36299=AXIS2_PLACEMENT_3D('',#81374,#45741,#45742) ;
#36300=AXIS2_PLACEMENT_3D('',#81375,#45743,#45744) ;
#36301=AXIS2_PLACEMENT_3D('',#81376,#45745,#45746) ;
#36302=AXIS2_PLACEMENT_3D('',#81377,#45747,#45748) ;
#36303=AXIS2_PLACEMENT_3D('',#81378,#45749,#45750) ;
#36304=AXIS2_PLACEMENT_3D('',#81389,#45757,#45758) ;
#36305=AXIS2_PLACEMENT_3D('',#81400,#45765,#45766) ;
#36306=AXIS2_PLACEMENT_3D('',#81411,#45773,#45774) ;
#36307=AXIS2_PLACEMENT_3D('',#81422,#45781,#45782) ;
#36308=AXIS2_PLACEMENT_3D('',#81423,#45783,#45784) ;
#36309=AXIS2_PLACEMENT_3D('',#81425,#45785,#45786) ;
#36310=AXIS2_PLACEMENT_3D('',#81426,#45787,#45788) ;
#36311=AXIS2_PLACEMENT_3D('',#81427,#45789,#45790) ;
#36312=AXIS2_PLACEMENT_3D('',#81428,#45791,#45792) ;
#36313=AXIS2_PLACEMENT_3D('',#81458,#45793,#45794) ;
#36314=AXIS2_PLACEMENT_3D('',#81471,#45795,#45796) ;
#36315=AXIS2_PLACEMENT_3D('',#81473,#45798,#45799) ;
#36316=AXIS2_PLACEMENT_3D('',#81504,#45801,#45802) ;
#36317=AXIS2_PLACEMENT_3D('',#81517,#45803,#45804) ;
#36318=AXIS2_PLACEMENT_3D('',#81519,#45806,#45807) ;
#36319=AXIS2_PLACEMENT_3D('',#81550,#45809,#45810) ;
#36320=AXIS2_PLACEMENT_3D('',#81589,#45811,#45812) ;
#36321=AXIS2_PLACEMENT_3D('',#81596,#45813,#45814) ;
#36322=AXIS2_PLACEMENT_3D('',#81598,#45816,#45817) ;
#36323=AXIS2_PLACEMENT_3D('',#81629,#45819,#45820) ;
#36324=AXIS2_PLACEMENT_3D('',#81642,#45821,#45822) ;
#36325=AXIS2_PLACEMENT_3D('',#81644,#45824,#45825) ;
#36326=AXIS2_PLACEMENT_3D('',#81646,#45827,#45828) ;
#36327=AXIS2_PLACEMENT_3D('',#81647,#45829,#45830) ;
#36328=AXIS2_PLACEMENT_3D('',#81648,#45831,#45832) ;
#36329=AXIS2_PLACEMENT_3D('',#81649,#45833,#45834) ;
#45330=DIRECTION('axis',(0.,0.,1.)) ;
#45331=DIRECTION('refdir',(1.,0.,0.)) ;
#45332=DIRECTION('center_axis',(7.71011961179131E-14,1.,-8.96434510032606E-14)) ;
#45333=DIRECTION('ref_axis',(-0.597896819887404,1.1795433654226E-13,0.801573073879437)) ;
#45334=DIRECTION('center_axis',(-5.25111655993446E-9,-1.,5.25108985668226E-9)) ;
#45335=DIRECTION('ref_axis',(-0.707106793325191,7.42618137461088E-9,0.707106769047904)) ;
#45336=DIRECTION('center_axis',(-1.73807139389439E-14,1.,1.64443783657369E-14)) ;
#45337=DIRECTION('ref_axis',(0.5978968198874,2.35732445061274E-14,-0.80157307387944)) ;
#45338=DIRECTION('center_axis',(2.0085626353944E-13,-1.,-1.93736401307529E-13)) ;
#45339=DIRECTION('ref_axis',(0.728572555974573,2.79041719628071E-13,-0.684968634815257)) ;
#45340=DIRECTION('center_axis',(2.7392192633255E-15,1.,-3.67555483654062E-15)) ;
#45341=DIRECTION('ref_axis',(-0.707106796087576,4.5359302518428E-15,0.707106766285518)) ;
#45342=DIRECTION('center_axis',(5.25109179432767E-9,-1.,-5.25111813730416E-9)) ;
#45343=DIRECTION('ref_axis',(-0.728572559766829,-7.42265259074552E-9,0.684968630781593)) ;
#45344=DIRECTION('center_axis',(1.35274044298125E-14,1.,5.65619335361478E-15)) ;
#45345=DIRECTION('ref_axis',(-0.801573073879436,1.42250231692097E-14,-0.597896819887406)) ;
#45346=DIRECTION('center_axis',(-4.03746661613741E-13,-1.,-3.97331887513712E-13)) ;
#45347=DIRECTION('ref_axis',(-0.684968634815258,5.66038908472849E-13,-0.728572555974572)) ;
#45348=DIRECTION('center_axis',(2.7392192633255E-15,1.,-3.67555483654062E-15)) ;
#45349=DIRECTION('ref_axis',(0.801573073879438,1.91814315580942E-18,0.597896819887403)) ;
#45350=DIRECTION('center_axis',(-2.06334705469751E-13,-1.,-1.9373640471103E-13)) ;
#45351=DIRECTION('ref_axis',(0.684968634815263,-2.82483829086263E-13,0.728572555974568)) ;
#45352=DIRECTION('center_axis',(-2.7392192633255E-15,-1.,3.67555483654062E-15)) ;
#45353=DIRECTION('ref_axis',(-2.02401438901654E-13,-3.67555483654007E-15,
-1.)) ;
#45354=DIRECTION('center_axis',(-2.7392192633255E-15,-1.,3.67555483654062E-15)) ;
#45355=DIRECTION('ref_axis',(-0.581108581115083,-1.3994784034356E-15,-0.813826036050958)) ;
#45356=DIRECTION('',(-2.7392192633255E-15,-1.,3.67555483654062E-15)) ;
#45357=DIRECTION('center_axis',(-2.17161023787667E-15,-1.,3.15364308176334E-15)) ;
#45358=DIRECTION('ref_axis',(-0.581108581115083,-1.30457550428349E-15,-0.813826036050958)) ;
#45359=DIRECTION('center_axis',(2.7392192633255E-15,1.,-3.67555483654062E-15)) ;
#45360=DIRECTION('ref_axis',(2.02476924116013E-13,3.67555483654007E-15,
1.)) ;
#45361=DIRECTION('',(1.,-2.73921926332625E-15,-2.02476924116013E-13)) ;
#45362=DIRECTION('',(2.02476924116013E-13,3.67555483654007E-15,1.)) ;
#45363=DIRECTION('center_axis',(2.73921926332383E-15,1.,-5.60637748192944E-15)) ;
#45364=DIRECTION('ref_axis',(1.,-2.73921926337039E-15,-8.30565686121179E-12)) ;
#45365=DIRECTION('',(-2.02476924116013E-13,-3.67555483654007E-15,-1.)) ;
#45366=DIRECTION('',(1.,-2.73921926332624E-15,-1.99806052959965E-13)) ;
#45367=DIRECTION('',(-2.02476924116013E-13,-3.67555483654007E-15,-1.)) ;
#45368=DIRECTION('',(1.,-2.73921926332625E-15,-2.02476924116013E-13)) ;
#45369=DIRECTION('center_axis',(1.77380794165008E-15,1.,-4.64096615924138E-15)) ;
#45370=DIRECTION('ref_axis',(-8.30613956687314E-12,-4.64096615922665E-15,
-1.)) ;
#45371=DIRECTION('',(-1.,2.73921926332625E-15,2.02476924116013E-13)) ;
#45372=DIRECTION('',(-2.02476924116013E-13,-3.67555483654007E-15,-1.)) ;
#45373=DIRECTION('',(-1.,2.73921926332625E-15,2.02476924116013E-13)) ;
#45374=DIRECTION('',(-2.02476924116013E-13,-3.67555483654007E-15,-1.)) ;
#45375=DIRECTION('center_axis',(2.73921926332384E-15,1.,-5.60637748192943E-15)) ;
#45376=DIRECTION('ref_axis',(-1.,2.73921926337041E-15,8.30662227253449E-12)) ;
#45377=DIRECTION('',(2.02476924116013E-13,3.67555483654007E-15,1.)) ;
#45378=DIRECTION('',(-1.,2.73921926332625E-15,2.02476924116013E-13)) ;
#45379=DIRECTION('',(2.02476924116013E-13,3.67555483654007E-15,1.)) ;
#45380=DIRECTION('',(-1.,2.73921926332625E-15,2.02476924116013E-13)) ;
#45381=DIRECTION('center_axis',(-1.12242602745208E-15,1.,-3.67555483653727E-15)) ;
#45382=DIRECTION('ref_axis',(8.31724179708421E-12,3.67555483654661E-15,
1.)) ;
#45383=DIRECTION('',(1.,-2.73921926332625E-15,-2.02476924116013E-13)) ;
#45384=DIRECTION('',(2.02476924116013E-13,3.67555483654007E-15,1.)) ;
#45385=DIRECTION('center_axis',(2.7392192633255E-15,1.,-3.67555483654062E-15)) ;
#45386=DIRECTION('ref_axis',(2.02476924116013E-13,3.67555483654007E-15,
1.)) ;
#45387=DIRECTION('',(-1.,2.73921926666159E-15,9.07642502817205E-10)) ;
#45388=DIRECTION('',(2.02476924116013E-13,3.67555483654007E-15,1.)) ;
#45389=DIRECTION('',(1.,-2.7392192599909E-15,9.07238034699055E-10)) ;
#45390=DIRECTION('center_axis',(-2.7392192633255E-15,-1.,3.67555483654062E-15)) ;
#45391=DIRECTION('ref_axis',(3.52629806639308E-11,-3.67555483663721E-15,
-1.)) ;
#45392=DIRECTION('center_axis',(2.7392192633255E-15,1.,-3.67555483654062E-15)) ;
#45393=DIRECTION('ref_axis',(2.02476924116013E-13,3.67555483654007E-15,
1.)) ;
#45394=DIRECTION('',(-2.02476924116013E-13,-3.67555483654007E-15,-1.)) ;
#45395=DIRECTION('',(-1.,2.7392192599909E-15,-9.0723803469906E-10)) ;
#45396=DIRECTION('center_axis',(-2.12242869659861E-15,-1.,4.29234540331102E-15)) ;
#45397=DIRECTION('ref_axis',(-3.52635974544975E-11,4.29234540338586E-15,
1.)) ;
#45398=DIRECTION('',(1.,-2.73921926666159E-15,-9.07642017093344E-10)) ;
#45399=DIRECTION('center_axis',(2.7392192633255E-15,1.,-3.67555483654062E-15)) ;
#45400=DIRECTION('ref_axis',(2.02476924116013E-13,3.67555483654007E-15,
1.)) ;
#45401=DIRECTION('',(9.07642017094632E-10,3.67555483405439E-15,1.)) ;
#45402=DIRECTION('',(1.,-2.73921926332625E-15,-2.02476924116013E-13)) ;
#45403=DIRECTION('',(9.07238034699055E-10,-3.67555483902575E-15,-1.)) ;
#45404=DIRECTION('center_axis',(-2.739219263369E-15,-1.,4.90913597003791E-15)) ;
#45405=DIRECTION('ref_axis',(-1.,2.73921926319589E-15,-3.5262363873364E-11)) ;
#45406=DIRECTION('center_axis',(2.7392192633255E-15,1.,-3.67555483654062E-15)) ;
#45407=DIRECTION('ref_axis',(2.02476924116013E-13,3.67555483654007E-15,
1.)) ;
#45408=DIRECTION('',(-1.,2.73921926332625E-15,2.02476924116013E-13)) ;
#45409=DIRECTION('',(-9.0723803469906E-10,3.67555483902575E-15,1.)) ;
#45410=DIRECTION('center_axis',(-2.7392192633255E-15,-1.,3.67555483654062E-15)) ;
#45411=DIRECTION('ref_axis',(1.,-2.73921926319589E-15,3.52629806639308E-11)) ;
#45412=DIRECTION('',(-9.07642988539774E-10,-3.67555483405439E-15,-1.)) ;
#45413=DIRECTION('center_axis',(6.99883249118274E-11,1.,4.68598587806925E-10)) ;
#45414=DIRECTION('ref_axis',(-2.06578141065567E-13,4.68605298162149E-10,
-1.)) ;
#45415=DIRECTION('center_axis',(-7.77996834011603E-11,2.60066914135082E-11,
1.)) ;
#45416=DIRECTION('ref_axis',(-1.,1.5214735684773E-8,-7.77996837968452E-11)) ;
#45417=DIRECTION('center_axis',(-2.86196449187501E-12,2.73622147742173E-12,
-1.)) ;
#45418=DIRECTION('ref_axis',(1.,1.38251899120395E-8,-2.86196445404623E-12)) ;
#45419=DIRECTION('center_axis',(2.7392192633255E-15,1.,-3.67555483654062E-15)) ;
#45420=DIRECTION('ref_axis',(-1.,2.7392192634357E-15,2.99814340021243E-11)) ;
#45421=DIRECTION('center_axis',(-2.02476924116013E-13,-3.67555483654007E-15,
-1.)) ;
#45422=DIRECTION('ref_axis',(-0.707106781186542,0.707106781186553,1.40573796326685E-13)) ;
#45423=DIRECTION('',(2.02476924116013E-13,3.67555483654007E-15,1.)) ;
#45424=DIRECTION('center_axis',(2.73952003670914E-13,-6.77995247183616E-14,
1.)) ;
#45425=DIRECTION('ref_axis',(-1.,-2.6866728060012E-14,2.73952003670912E-13)) ;
#45426=DIRECTION('center_axis',(2.02476924116013E-13,3.67555483654007E-15,
1.)) ;
#45427=DIRECTION('ref_axis',(0.707106781186549,0.707106781186546,-1.45771815825768E-13)) ;
#45428=DIRECTION('center_axis',(2.02476924116013E-13,3.67555483654007E-15,
1.)) ;
#45429=DIRECTION('ref_axis',(-2.40911704984497E-14,1.,-3.67555483653519E-15)) ;
#45430=DIRECTION('',(-2.02476924116013E-13,-3.67555483654007E-15,-1.)) ;
#45431=DIRECTION('center_axis',(4.68612409773722E-10,1.,-6.99878726045723E-11)) ;
#45432=DIRECTION('ref_axis',(-2.06578141065567E-13,-6.99783452859607E-11,
-1.)) ;
#45433=DIRECTION('center_axis',(-1.,2.60157134512408E-11,-2.57836941530287E-11)) ;
#45434=DIRECTION('ref_axis',(2.6015713512402E-11,1.,-2.37208950382905E-9)) ;
#45435=DIRECTION('center_axis',(-1.,2.8805387413756E-12,2.79437612800868E-12)) ;
#45436=DIRECTION('ref_axis',(-2.79437608818469E-12,1.38251889757039E-8,
-1.)) ;
#45437=DIRECTION('center_axis',(5.18773214108251E-16,1.,-3.67555483650711E-15)) ;
#45438=DIRECTION('ref_axis',(2.99814340021243E-11,3.67555483649156E-15,
1.)) ;
#45439=DIRECTION('center_axis',(-1.,2.73921926332625E-15,2.02476924116013E-13)) ;
#45440=DIRECTION('ref_axis',(1.4510972659248E-13,0.707106781186553,0.707106781186542)) ;
#45441=DIRECTION('',(1.,-2.73921926332625E-15,-2.02476924116013E-13)) ;
#45442=DIRECTION('center_axis',(1.,-7.42142988182295E-14,-2.73952003670916E-13)) ;
#45443=DIRECTION('ref_axis',(2.73952003670915E-13,-1.11274188251291E-14,
1.)) ;
#45444=DIRECTION('center_axis',(1.,-2.77538307019574E-15,-2.0249012323252E-13)) ;
#45445=DIRECTION('ref_axis',(-1.4121964707169E-13,0.707106781186544,-0.707106781186551)) ;
#45446=DIRECTION('center_axis',(1.,-1.2782060848441E-13,-7.73955348949296E-14)) ;
#45447=DIRECTION('ref_axis',(1.2782060848441E-13,1.,1.87556028655978E-15)) ;
#45448=DIRECTION('',(-1.,2.73921926332625E-15,2.02476924116013E-13)) ;
#45449=DIRECTION('center_axis',(-6.99814578304714E-11,1.,-4.68613346109296E-10)) ;
#45450=DIRECTION('ref_axis',(4.44143003290968E-12,4.68622513007238E-10,
1.)) ;
#45451=DIRECTION('center_axis',(7.77280223498716E-11,2.59905918894472E-11,
-1.)) ;
#45452=DIRECTION('ref_axis',(1.,1.52147302063345E-8,7.77280227453114E-11)) ;
#45453=DIRECTION('center_axis',(2.94237395572288E-12,2.66316312194452E-12,
1.)) ;
#45454=DIRECTION('ref_axis',(-1.,1.38252397993977E-8,2.94237391890401E-12)) ;
#45455=DIRECTION('center_axis',(2.739219263359E-15,1.,-1.45510878732336E-15)) ;
#45456=DIRECTION('ref_axis',(1.,-2.73921926340261E-15,-2.9971997106415E-11)) ;
#45457=DIRECTION('center_axis',(2.02476924116013E-13,3.67555483654007E-15,
1.)) ;
#45458=DIRECTION('ref_axis',(0.707106781186548,0.707106781186547,-1.45771815825767E-13)) ;
#45459=DIRECTION('',(-2.02476924116013E-13,-3.67555483654007E-15,-1.)) ;
#45460=DIRECTION('center_axis',(-2.73952003670918E-13,-7.51506343914451E-14,
-1.)) ;
#45461=DIRECTION('ref_axis',(1.,-2.73921926332633E-15,-2.73952003670918E-13)) ;
#45462=DIRECTION('center_axis',(-2.02476924116013E-13,-3.67555483654007E-15,
-1.)) ;
#45463=DIRECTION('ref_axis',(-0.707106781186546,0.707106781186549,1.40573796326686E-13)) ;
#45464=DIRECTION('center_axis',(-2.02476924116013E-13,-3.67555483654007E-15,
-1.)) ;
#45465=DIRECTION('ref_axis',(-1.94652412291771E-14,1.,-3.67555483653613E-15)) ;
#45466=DIRECTION('',(2.02476924116013E-13,3.67555483654007E-15,1.)) ;
#45467=DIRECTION('center_axis',(1.,-2.73921926332625E-15,-2.02476924116013E-13)) ;
#45468=DIRECTION('ref_axis',(-2.73921926332551E-15,-1.,3.67555483654063E-15)) ;
#45469=DIRECTION('',(-2.02476924116013E-13,-3.67555483654007E-15,-1.)) ;
#45470=DIRECTION('',(-2.7392192633255E-15,-1.,3.67555483654062E-15)) ;
#45471=DIRECTION('',(-2.7392192633255E-15,-1.,3.67555483654062E-15)) ;
#45472=DIRECTION('center_axis',(-1.,2.73921926332625E-15,2.02476924116013E-13)) ;
#45473=DIRECTION('ref_axis',(2.73921926332551E-15,1.,-3.67555483654063E-15)) ;
#45474=DIRECTION('',(2.02476924116013E-13,3.67555483654007E-15,1.)) ;
#45475=DIRECTION('',(-2.73921924526551E-15,-1.,8.91989933532196E-11)) ;
#45476=DIRECTION('',(-2.7392192633255E-15,-1.,3.67555483654062E-15)) ;
#45477=DIRECTION('center_axis',(-2.7392192633255E-15,-1.,3.67555483654062E-15)) ;
#45478=DIRECTION('ref_axis',(1.,-2.73921926332624E-15,-2.02476924116013E-13)) ;
#45479=DIRECTION('center_axis',(-2.7392192633255E-15,-1.,3.67555483654062E-15)) ;
#45480=DIRECTION('ref_axis',(-1.,2.73921926332625E-15,2.03032035628326E-13)) ;
#45481=DIRECTION('center_axis',(-2.02476924116013E-13,-3.67555483654007E-15,
-1.)) ;
#45482=DIRECTION('ref_axis',(-0.707106781186547,-0.707106781186548,1.45771815825767E-13)) ;
#45483=DIRECTION('center_axis',(-1.73057417312571E-11,1.71934002942205E-11,
-1.)) ;
#45484=DIRECTION('ref_axis',(-1.,1.54909559440142E-8,1.73057419975993E-11)) ;
#45485=DIRECTION('center_axis',(1.22067459616746E-13,-7.67339096627288E-14,
1.)) ;
#45486=DIRECTION('ref_axis',(4.19967464056558E-15,-1.,-7.67339096627293E-14)) ;
#45487=DIRECTION('center_axis',(2.0247579896626E-13,3.65514229881304E-15,
1.)) ;
#45488=DIRECTION('ref_axis',(0.707106781186545,-0.70710678118655,-1.40587434569514E-13)) ;
#45489=DIRECTION('center_axis',(2.02476924116013E-13,3.67555483654007E-15,
1.)) ;
#45490=DIRECTION('ref_axis',(1.,1.94652412291775E-14,-2.02476924116013E-13)) ;
#45491=DIRECTION('center_axis',(2.45592326533471E-10,-7.36846277275853E-11,
1.)) ;
#45492=DIRECTION('ref_axis',(1.,1.70479272859721E-8,-2.45592325277301E-10)) ;
#45493=DIRECTION('center_axis',(-6.68032841410509E-11,-1.,4.47277340551685E-10)) ;
#45494=DIRECTION('ref_axis',(1.79034390085963E-13,4.47295044331018E-10,
1.)) ;
#45495=DIRECTION('center_axis',(-2.02476924116013E-13,-3.67555483654007E-15,
-1.)) ;
#45496=DIRECTION('ref_axis',(-2.7392192633255E-15,-1.,3.67555483654062E-15)) ;
#45497=DIRECTION('',(-2.7392192633255E-15,-1.,3.67555483654062E-15)) ;
#45498=DIRECTION('',(-1.,2.73921926332625E-15,2.02476924116013E-13)) ;
#45499=DIRECTION('',(-2.7392192633255E-15,-1.,3.67555483654062E-15)) ;
#45500=DIRECTION('',(-1.,2.73921926332625E-15,2.02476924116013E-13)) ;
#45501=DIRECTION('center_axis',(2.02476924116013E-13,3.67555483654007E-15,
1.)) ;
#45502=DIRECTION('ref_axis',(2.7392192633255E-15,1.,-3.67555483654062E-15)) ;
#45503=DIRECTION('',(-2.7392192633255E-15,-1.,3.67555483654062E-15)) ;
#45504=DIRECTION('',(1.,-2.73921926332625E-15,-2.02476924116013E-13)) ;
#45505=DIRECTION('',(1.70194450455769E-10,-1.,3.67555480207962E-15)) ;
#45506=DIRECTION('',(1.,-2.73921926332625E-15,-2.02476924116013E-13)) ;
#45507=DIRECTION('center_axis',(4.47280390523803E-10,-1.,6.68024460996793E-11)) ;
#45508=DIRECTION('ref_axis',(1.79034390085955E-13,6.68245860995827E-11,
1.)) ;
#45509=DIRECTION('center_axis',(-1.,-7.98040177460166E-11,7.999583231198E-11)) ;
#45510=DIRECTION('ref_axis',(7.98040175334014E-11,-1.,-2.65782865320679E-9)) ;
#45511=DIRECTION('center_axis',(-1.,1.72095703729976E-11,1.73959065004325E-11)) ;
#45512=DIRECTION('ref_axis',(1.7395906767025E-11,1.54909457781191E-8,1.)) ;
#45513=DIRECTION('center_axis',(-2.7392192633255E-15,-1.,3.67555483654062E-15)) ;
#45514=DIRECTION('ref_axis',(2.03032035628326E-13,3.67555483654006E-15,
1.)) ;
#45515=DIRECTION('center_axis',(-1.,2.73921926332625E-15,2.02476924116013E-13)) ;
#45516=DIRECTION('ref_axis',(1.41235885559973E-13,-0.707106781186544,0.707106781186551)) ;
#45517=DIRECTION('center_axis',(1.,-2.95423740964165E-14,-1.75673769282923E-13)) ;
#45518=DIRECTION('ref_axis',(-2.95423740964141E-14,-1.,1.33900063020159E-14)) ;
#45519=DIRECTION('center_axis',(1.,-2.73921926332625E-15,-2.02476924116013E-13)) ;
#45520=DIRECTION('ref_axis',(-1.45109726592481E-13,-0.707106781186552,-0.707106781186543)) ;
#45521=DIRECTION('center_axis',(1.,-2.73921926332625E-15,-2.02476924116013E-13)) ;
#45522=DIRECTION('ref_axis',(-2.02476924116013E-13,-3.67555483654007E-15,
-1.)) ;
#45523=DIRECTION('center_axis',(-1.,2.73921926332625E-15,2.02476924116013E-13)) ;
#45524=DIRECTION('ref_axis',(2.73921926332551E-15,1.,-3.67555483654063E-15)) ;
#45525=DIRECTION('',(2.02476924116013E-13,3.67555483654007E-15,1.)) ;
#45526=DIRECTION('',(-2.7392192633255E-15,-1.,3.67555483654062E-15)) ;
#45527=DIRECTION('',(-2.7392192633255E-15,-1.,3.67555483654062E-15)) ;
#45528=DIRECTION('center_axis',(1.,-2.73921926332625E-15,-2.02476924116013E-13)) ;
#45529=DIRECTION('ref_axis',(-2.73921926332551E-15,-1.,3.67555483654063E-15)) ;
#45530=DIRECTION('',(-2.02476924116013E-13,-3.67555483654007E-15,-1.)) ;
#45531=DIRECTION('',(-2.7392192813855E-15,-1.,-8.91916422435465E-11)) ;
#45532=DIRECTION('',(-2.7392192633255E-15,-1.,3.67555483654062E-15)) ;
#45533=DIRECTION('center_axis',(-2.7392192633255E-15,-1.,3.67555483654062E-15)) ;
#45534=DIRECTION('ref_axis',(-1.,2.73921926332624E-15,2.02476924116013E-13)) ;
#45535=DIRECTION('center_axis',(-2.7392192633255E-15,-1.,3.67555483654062E-15)) ;
#45536=DIRECTION('ref_axis',(1.,-2.73921926332625E-15,-2.04142258652951E-13)) ;
#45537=DIRECTION('center_axis',(6.67961373153174E-11,-1.,-4.47275108033656E-10)) ;
#45538=DIRECTION('ref_axis',(5.41579030010014E-12,4.47272665032237E-10,
-1.)) ;
#45539=DIRECTION('center_axis',(8.60965078876547E-11,-8.59037569861192E-11,
1.)) ;
#45540=DIRECTION('ref_axis',(-2.65783506798089E-9,-1.,-8.59037567572889E-11)) ;
#45541=DIRECTION('center_axis',(1.73959065004326E-11,1.72105067085707E-11,
1.)) ;
#45542=DIRECTION('ref_axis',(1.,1.5490939363345E-8,-1.73959067670395E-11)) ;
#45543=DIRECTION('center_axis',(2.02476924116013E-13,3.67555483654007E-15,
1.)) ;
#45544=DIRECTION('ref_axis',(0.707106781186546,-0.707106781186549,-1.40573796326686E-13)) ;
#45545=DIRECTION('center_axis',(-1.75673769282924E-13,-3.04787096696305E-14,
-1.)) ;
#45546=DIRECTION('ref_axis',(6.97523220214981E-15,-1.,3.04787096696293E-14)) ;
#45547=DIRECTION('center_axis',(-2.02476924116013E-13,-3.67555483654007E-15,
-1.)) ;
#45548=DIRECTION('ref_axis',(-0.707106781186547,-0.707106781186548,1.45771815825767E-13)) ;
#45549=DIRECTION('center_axis',(-2.02476924116013E-13,-3.67555483654007E-15,
-1.)) ;
#45550=DIRECTION('ref_axis',(-1.,-1.94652412291768E-14,2.02476924116013E-13)) ;
#45551=DIRECTION('center_axis',(2.02476924116013E-13,3.67555483654007E-15,
1.)) ;
#45552=DIRECTION('ref_axis',(2.7392192633255E-15,1.,-3.67555483654062E-15)) ;
#45553=DIRECTION('',(1.,-2.73921926332625E-15,-2.02476924116013E-13)) ;
#45554=DIRECTION('',(-2.7392192633255E-15,-1.,3.67555483654062E-15)) ;
#45555=DIRECTION('',(-2.7392192633255E-15,-1.,3.67555483654062E-15)) ;
#45556=DIRECTION('center_axis',(-2.02476924116013E-13,-3.67555483654007E-15,
-1.)) ;
#45557=DIRECTION('ref_axis',(-2.7392192633255E-15,-1.,3.67555483654062E-15)) ;
#45558=DIRECTION('',(-1.,2.73921926332625E-15,2.02476924116013E-13)) ;
#45559=DIRECTION('',(-8.91980570176463E-11,-1.,3.67555485460062E-15)) ;
#45560=DIRECTION('',(-2.7392192633255E-15,-1.,3.67555483654062E-15)) ;
#45561=DIRECTION('center_axis',(-2.7392192633255E-15,-1.,3.67555483654062E-15)) ;
#45562=DIRECTION('ref_axis',(2.02476924116013E-13,3.67555483654007E-15,
1.)) ;
#45563=DIRECTION('center_axis',(-2.7392192633255E-15,-1.,3.67555483654062E-15)) ;
#45564=DIRECTION('ref_axis',(-2.03032035628326E-13,-3.67555483654006E-15,
-1.)) ;
#45565=DIRECTION('center_axis',(1.,-2.73921926332625E-15,-2.02476924116013E-13)) ;
#45566=DIRECTION('ref_axis',(-1.45109726592481E-13,-0.707106781186552,-0.707106781186543)) ;
#45567=DIRECTION('center_axis',(1.,1.71943366297936E-11,-1.73057417312572E-11)) ;
#45568=DIRECTION('ref_axis',(-1.73057419976138E-11,1.54909495292401E-8,
-1.)) ;
#45569=DIRECTION('center_axis',(-1.,2.73921926332625E-15,2.02476924116013E-13)) ;
#45570=DIRECTION('ref_axis',(-2.7392192633241E-15,-1.,1.06144487404478E-14)) ;
#45571=DIRECTION('center_axis',(-1.,2.71880672559922E-15,2.0247579896626E-13)) ;
#45572=DIRECTION('ref_axis',(1.412495238028E-13,-0.707106781186546,0.707106781186549)) ;
#45573=DIRECTION('center_axis',(-1.,2.73921926332625E-15,2.02476924116013E-13)) ;
#45574=DIRECTION('ref_axis',(2.02476924116013E-13,1.47777850827919E-14,
1.)) ;
#45575=DIRECTION('center_axis',(-1.,-7.3685564063157E-11,2.45592326533472E-10)) ;
#45576=DIRECTION('ref_axis',(2.45592325277285E-10,1.70479337007462E-8,1.)) ;
#45577=DIRECTION('center_axis',(-4.4727640421611E-10,-1.,-6.67968693669511E-11)) ;
#45578=DIRECTION('ref_axis',(1.79034390085963E-13,-6.67798275020642E-11,
1.)) ;
#45579=DIRECTION('center_axis',(-2.7392192633255E-15,-1.,3.67555483654062E-15)) ;
#45580=DIRECTION('ref_axis',(-2.02476924116013E-13,-3.67555483654007E-15,
-1.)) ;
#45581=DIRECTION('center_axis',(4.95966531254277E-15,1.,-3.67555483657413E-15)) ;
#45582=DIRECTION('ref_axis',(-2.9971997106415E-11,-3.67555483642548E-15,
-1.)) ;
#45583=DIRECTION('center_axis',(-4.68606931335196E-10,1.,6.99805214948982E-11)) ;
#45584=DIRECTION('ref_axis',(-2.06578141065567E-13,6.99783452859607E-11,
-1.)) ;
#45585=DIRECTION('center_axis',(1.,2.60638413228166E-11,2.57300878437945E-11)) ;
#45586=DIRECTION('ref_axis',(-2.60638413838492E-11,1.,2.3720331178697E-9)) ;
#45587=DIRECTION('center_axis',(1.,2.66568273286117E-12,-2.93343957085108E-12)) ;
#45588=DIRECTION('ref_axis',(2.93343953399749E-12,1.38251963268136E-8,1.)) ;
#45589=DIRECTION('center_axis',(1.,-2.70940101215817E-15,-2.02507881810474E-13)) ;
#45590=DIRECTION('ref_axis',(-1.41278860643259E-13,0.70710678118655,-0.707106781186545)) ;
#45591=DIRECTION('center_axis',(-1.,-5.08670904028541E-14,2.56083233782194E-13)) ;
#45592=DIRECTION('ref_axis',(-2.56083233782195E-13,2.5930392486797E-14,
-1.)) ;
#45593=DIRECTION('center_axis',(-1.,2.73921926332625E-15,2.02476924116013E-13)) ;
#45594=DIRECTION('ref_axis',(1.45109726592481E-13,0.707106781186551,0.707106781186544)) ;
#45595=DIRECTION('center_axis',(-1.,2.73921926332625E-15,2.02476924116013E-13)) ;
#45596=DIRECTION('ref_axis',(2.73921926332007E-15,1.,-3.05059445983158E-14)) ;
#45597=DIRECTION('center_axis',(-2.7392192633255E-15,-1.,3.67555483654062E-15)) ;
#45598=DIRECTION('ref_axis',(-2.02476924116013E-13,-3.67555483654007E-15,
-1.)) ;
#45599=DIRECTION('center_axis',(-2.7392192633255E-15,-1.,3.67555483654062E-15)) ;
#45600=DIRECTION('ref_axis',(-2.02476924116013E-13,-3.67555483654007E-15,
-1.)) ;
#45601=DIRECTION('',(1.,-2.73921926332625E-15,-2.0199120154274E-13)) ;
#45602=DIRECTION('',(2.02476924116013E-13,3.67555483654007E-15,1.)) ;
#45603=DIRECTION('',(-1.,2.73921926332625E-15,2.0199120154274E-13)) ;
#45604=DIRECTION('center_axis',(-2.02476924116013E-13,-3.67555483654007E-15,
-1.)) ;
#45605=DIRECTION('ref_axis',(-2.7392192633255E-15,-1.,3.67555483654062E-15)) ;
#45606=DIRECTION('',(1.,-2.73921926332625E-15,-2.02476924116013E-13)) ;
#45607=DIRECTION('',(8.87904497774877E-12,-1.,3.67555483474227E-15)) ;
#45608=DIRECTION('',(1.,-2.18410775101367E-15,-2.02546313055052E-13)) ;
#45609=DIRECTION('center_axis',(2.02476924116013E-13,3.67555483654007E-15,
1.)) ;
#45610=DIRECTION('ref_axis',(2.7392192633255E-15,1.,-3.67555483654062E-15)) ;
#45611=DIRECTION('',(-2.73921926312881E-15,-1.,9.75120701384738E-13)) ;
#45612=DIRECTION('',(-1.,2.73921926332625E-15,2.02962646689287E-13)) ;
#45613=DIRECTION('',(-2.7392192633255E-15,-1.,3.67555483654062E-15)) ;
#45614=DIRECTION('',(-1.,2.73921926332625E-15,2.02476924116013E-13)) ;
#45615=DIRECTION('center_axis',(2.7392192633255E-15,1.,-3.67555483654062E-15)) ;
#45616=DIRECTION('ref_axis',(-1.,2.73921926332625E-15,2.02673185673349E-13)) ;
#45617=DIRECTION('center_axis',(-2.7392192633255E-15,-1.,3.67555483654062E-15)) ;
#45618=DIRECTION('ref_axis',(-1.,2.73921926332625E-15,2.02673185673349E-13)) ;
#45619=DIRECTION('center_axis',(-1.62899623870035E-15,-1.,3.6755548365404E-15)) ;
#45620=DIRECTION('ref_axis',(-2.01921812603701E-13,-3.67555483654007E-15,
-1.)) ;
#45621=DIRECTION('center_axis',(-1.,2.73921926332625E-15,2.02476924116013E-13)) ;
#45622=DIRECTION('ref_axis',(-2.02476924116013E-13,-3.67555483654007E-15,
-1.)) ;
#45623=DIRECTION('center_axis',(1.,2.72296279542125E-14,-1.42803113028906E-13)) ;
#45624=DIRECTION('ref_axis',(-1.42803113028906E-13,-3.67555483654022E-15,
-1.)) ;
#45625=DIRECTION('center_axis',(-1.,-2.9385320195592E-15,1.63381088479862E-13)) ;
#45626=DIRECTION('ref_axis',(2.9385320195601E-15,-1.,5.53211507838757E-15)) ;
#45627=DIRECTION('center_axis',(1.,-2.73921926332625E-15,-2.02476924116013E-13)) ;
#45628=DIRECTION('ref_axis',(2.02476924116013E-13,3.67555483654007E-15,
1.)) ;
#45629=DIRECTION('center_axis',(1.,-7.22135217855854E-15,-1.97994791200781E-13)) ;
#45630=DIRECTION('ref_axis',(-7.2213521785591E-15,-1.,-2.82240600992682E-15)) ;
#45631=DIRECTION('center_axis',(1.,-2.73921926332625E-15,-2.02476924116013E-13)) ;
#45632=DIRECTION('ref_axis',(-2.73921926332635E-15,-1.,-5.017057076176E-16)) ;
#45633=DIRECTION('center_axis',(6.56896527721512E-15,1.,-4.97129876952025E-15)) ;
#45634=DIRECTION('ref_axis',(-1.79034390112784E-13,0.,-1.)) ;
#45635=DIRECTION('center_axis',(-2.7392192633255E-15,-1.,3.67555483654062E-15)) ;
#45636=DIRECTION('ref_axis',(-2.02476924116013E-13,-3.67555483654007E-15,
-1.)) ;
#45637=DIRECTION('center_axis',(-2.7392192633255E-15,-1.,3.67555483654062E-15)) ;
#45638=DIRECTION('ref_axis',(-1.,2.73921926332624E-15,2.02476924116013E-13)) ;
#45639=DIRECTION('',(-2.0199120154274E-13,-3.67555483654007E-15,-1.)) ;
#45640=DIRECTION('',(1.,-2.73921926332625E-15,-2.02476924116013E-13)) ;
#45641=DIRECTION('',(2.0199120154274E-13,3.67555483654007E-15,1.)) ;
#45642=DIRECTION('center_axis',(-1.,2.73921926332625E-15,2.02476924116013E-13)) ;
#45643=DIRECTION('ref_axis',(2.73921926332551E-15,1.,-3.67555483654063E-15)) ;
#45644=DIRECTION('',(-2.02476924116013E-13,-3.67555483654007E-15,-1.)) ;
#45645=DIRECTION('',(-2.73921926512386E-15,-1.,-8.87810864217555E-12)) ;
#45646=DIRECTION('',(-2.02546313055052E-13,-3.12044332422749E-15,-1.)) ;
#45647=DIRECTION('center_axis',(1.,-2.73921926332625E-15,-2.02476924116013E-13)) ;
#45648=DIRECTION('ref_axis',(-2.73921926332551E-15,-1.,3.67555483654063E-15)) ;
#45649=DIRECTION('',(9.68705927284872E-13,-1.,3.67555483634393E-15)) ;
#45650=DIRECTION('',(2.02962646689287E-13,3.67555483654007E-15,1.)) ;
#45651=DIRECTION('',(-2.7392192633255E-15,-1.,3.67555483654062E-15)) ;
#45652=DIRECTION('',(2.02476924116013E-13,3.67555483654007E-15,1.)) ;
#45653=DIRECTION('center_axis',(2.7392192633255E-15,1.,-3.67555483654062E-15)) ;
#45654=DIRECTION('ref_axis',(2.02673185673349E-13,3.67555483654006E-15,
1.)) ;
#45655=DIRECTION('center_axis',(-2.7392192633255E-15,-1.,3.67555483654062E-15)) ;
#45656=DIRECTION('ref_axis',(2.02673185673349E-13,3.67555483654006E-15,
1.)) ;
#45657=DIRECTION('center_axis',(-2.73921926332573E-15,-1.,2.56533181191547E-15)) ;
#45658=DIRECTION('ref_axis',(-1.,2.73921926332625E-15,2.01921812603701E-13)) ;
#45659=DIRECTION('center_axis',(2.02476924116013E-13,3.67555483654007E-15,
1.)) ;
#45660=DIRECTION('ref_axis',(-1.,2.73921926332625E-15,2.02476924116013E-13)) ;
#45661=DIRECTION('center_axis',(-1.42803113028906E-13,2.62932923809983E-14,
-1.)) ;
#45662=DIRECTION('ref_axis',(-1.,2.73921926332604E-15,1.42803113028906E-13)) ;
#45663=DIRECTION('center_axis',(1.63381088479862E-13,-2.00219644634513E-15,
1.)) ;
#45664=DIRECTION('ref_axis',(-8.82659021478556E-16,-1.,-2.00219644634499E-15)) ;
#45665=DIRECTION('center_axis',(-2.02476924116013E-13,-3.67555483654007E-15,
-1.)) ;
#45666=DIRECTION('ref_axis',(1.,-2.73921926332625E-15,-2.02476924116013E-13)) ;
#45667=DIRECTION('center_axis',(-1.97994791200781E-13,-8.15768775177239E-15,
-1.)) ;
#45668=DIRECTION('ref_axis',(-9.23718010979295E-15,-1.,8.15768775177422E-15)) ;
#45669=DIRECTION('center_axis',(-2.02476924116013E-13,-3.67555483654007E-15,
-1.)) ;
#45670=DIRECTION('ref_axis',(-6.91647980748373E-15,-1.,3.67555483654147E-15)) ;
#45671=DIRECTION('center_axis',(1.44347533034587E-15,1.,-7.50530085043024E-15)) ;
#45672=DIRECTION('ref_axis',(1.79034390112784E-13,0.,1.)) ;
#45673=DIRECTION('center_axis',(-2.7392192633255E-15,-1.,3.67555483654062E-15)) ;
#45674=DIRECTION('ref_axis',(-2.02476924116013E-13,-3.67555483654007E-15,
-1.)) ;
#45675=DIRECTION('',(-2.03032035628326E-13,-3.67555483654007E-15,-1.)) ;
#45676=DIRECTION('',(1.,-2.73921926332625E-15,-2.02476924116013E-13)) ;
#45677=DIRECTION('',(2.02962646689287E-13,3.67555483654007E-15,1.)) ;
#45678=DIRECTION('center_axis',(2.7392192633255E-15,1.,-3.67555483654062E-15)) ;
#45679=DIRECTION('ref_axis',(-1.,2.73921926332624E-15,2.02476924116013E-13)) ;
#45680=DIRECTION('center_axis',(-1.,2.73921926332625E-15,2.02476924116013E-13)) ;
#45681=DIRECTION('ref_axis',(2.73921926332551E-15,1.,-3.67555483654063E-15)) ;
#45682=DIRECTION('',(2.02823868811209E-13,4.23066634885265E-15,1.)) ;
#45683=DIRECTION('',(9.6870592728667E-13,-1.,8.88545975184844E-12)) ;
#45684=DIRECTION('',(-2.02476924116013E-13,-3.67555483654007E-15,-1.)) ;
#45685=DIRECTION('center_axis',(1.,-2.73921926332625E-15,-2.02476924116013E-13)) ;
#45686=DIRECTION('ref_axis',(-2.73921926332551E-15,-1.,3.67555483654063E-15)) ;
#45687=DIRECTION('',(-2.02476924116013E-13,-3.67555483654007E-15,-1.)) ;
#45688=DIRECTION('',(-2.7392192633255E-15,-1.,3.67555483654062E-15)) ;
#45689=DIRECTION('',(2.02476924116013E-13,3.67555483654007E-15,1.)) ;
#45690=DIRECTION('',(-2.7392192633255E-15,-1.,3.67555483654062E-15)) ;
#45691=DIRECTION('center_axis',(2.7392192633255E-15,1.,-3.67555483654062E-15)) ;
#45692=DIRECTION('ref_axis',(1.,-2.73921926332624E-15,-2.02476924116013E-13)) ;
#45693=DIRECTION('center_axis',(2.7392192633255E-15,1.,-3.67555483654062E-15)) ;
#45694=DIRECTION('ref_axis',(-1.,2.73921926332625E-15,2.03032035628326E-13)) ;
#45695=DIRECTION('center_axis',(-2.7392192633255E-15,-1.,3.67555483654062E-15)) ;
#45696=DIRECTION('ref_axis',(1.,-2.73921926332624E-15,-2.02476924116013E-13)) ;
#45697=DIRECTION('center_axis',(-2.02935662438468E-13,-3.51738227745041E-15,
-1.)) ;
#45698=DIRECTION('ref_axis',(-0.707106781186548,-0.707106781186547,1.45984347915236E-13)) ;
#45699=DIRECTION('center_axis',(2.28126356985122E-13,-4.09309664761724E-15,
1.)) ;
#45700=DIRECTION('ref_axis',(-8.82659021478992E-16,-1.,-4.09309664761704E-15)) ;
#45701=DIRECTION('center_axis',(-2.62150735203121E-13,-3.36444020540783E-14,
-1.)) ;
#45702=DIRECTION('ref_axis',(-1.,6.45233974702268E-15,2.62150735203121E-13)) ;
#45703=DIRECTION('center_axis',(2.02476924116013E-13,3.67555483654007E-15,
1.)) ;
#45704=DIRECTION('ref_axis',(0.707106781186545,-0.70710678118655,-1.40573796326686E-13)) ;
#45705=DIRECTION('center_axis',(-2.02476924116013E-13,-3.67555483654007E-15,
-1.)) ;
#45706=DIRECTION('ref_axis',(-4.13163944471158E-15,-1.,3.67555483654091E-15)) ;
#45707=DIRECTION('center_axis',(-2.06959057031246E-13,8.06578078692253E-16,
-1.)) ;
#45708=DIRECTION('ref_axis',(-6.91647980748464E-15,-1.,-8.06578078690822E-16)) ;
#45709=DIRECTION('center_axis',(3.74218483200288E-15,1.,-4.17141315729775E-15)) ;
#45710=DIRECTION('ref_axis',(-1.79034390112784E-13,0.,-1.)) ;
#45711=DIRECTION('center_axis',(-2.7392192633255E-15,-1.,3.67555483654062E-15)) ;
#45712=DIRECTION('ref_axis',(-2.02476924116013E-13,-3.67555483654007E-15,
-1.)) ;
#45713=DIRECTION('',(1.,-2.73921926332625E-15,-2.02476924116013E-13)) ;
#45714=DIRECTION('',(2.02476924116013E-13,3.67555483654007E-15,1.)) ;
#45715=DIRECTION('',(-1.,2.73921926332625E-15,2.02476924116013E-13)) ;
#45716=DIRECTION('center_axis',(2.7392192633255E-15,1.,-3.67555483654062E-15)) ;
#45717=DIRECTION('ref_axis',(-2.02476924116013E-13,-3.67555483654007E-15,
-1.)) ;
#45718=DIRECTION('center_axis',(-2.02476924116013E-13,-3.67555483654007E-15,
-1.)) ;
#45719=DIRECTION('ref_axis',(-2.7392192633255E-15,-1.,3.67555483654062E-15)) ;
#45720=DIRECTION('',(-1.,3.29433077563883E-15,2.02407535176974E-13)) ;
#45721=DIRECTION('',(-8.88452341627542E-12,-1.,3.67555483833898E-15)) ;
#45722=DIRECTION('',(1.,-2.73921926332625E-15,-2.02476924116013E-13)) ;
#45723=DIRECTION('center_axis',(2.01505478969466E-13,3.67555483654007E-15,
1.)) ;
#45724=DIRECTION('ref_axis',(2.7392192633255E-15,1.,-3.67555483654062E-15)) ;
#45725=DIRECTION('',(1.,-2.73921926332625E-15,-2.0199120154274E-13)) ;
#45726=DIRECTION('',(-2.7392192633255E-15,-1.,3.67555483654062E-15)) ;
#45727=DIRECTION('',(-1.,2.73921926332625E-15,2.02476924116013E-13)) ;
#45728=DIRECTION('',(-2.7392192635222E-15,-1.,-9.67769591711657E-13)) ;
#45729=DIRECTION('center_axis',(2.7392192633255E-15,1.,-3.67555483654062E-15)) ;
#45730=DIRECTION('ref_axis',(2.02476924116013E-13,3.67555483654007E-15,
1.)) ;
#45731=DIRECTION('center_axis',(2.7392192633255E-15,1.,-3.67555483654062E-15)) ;
#45732=DIRECTION('ref_axis',(-2.02476924116013E-13,-3.67555483654007E-15,
-1.)) ;
#45733=DIRECTION('center_axis',(-2.7392192633255E-15,-1.,3.67555483654062E-15)) ;
#45734=DIRECTION('ref_axis',(2.02476924116013E-13,3.67555483654007E-15,
1.)) ;
#45735=DIRECTION('center_axis',(1.,-2.55781860456987E-15,-2.02516882062598E-13)) ;
#45736=DIRECTION('ref_axis',(-1.45009711491555E-13,-0.70710678118655,-0.707106781186545)) ;
#45737=DIRECTION('center_axis',(-1.,-9.51156647651177E-15,2.23644222729441E-13)) ;
#45738=DIRECTION('ref_axis',(9.51156647651311E-15,-1.,5.99625513884829E-15)) ;
#45739=DIRECTION('center_axis',(1.,-3.2708066480865E-14,-2.62150735203121E-13)) ;
#45740=DIRECTION('ref_axis',(-2.62150735203121E-13,3.75656471563051E-17,
-1.)) ;
#45741=DIRECTION('center_axis',(-1.,2.58104670423658E-15,2.02018185793558E-13)) ;
#45742=DIRECTION('ref_axis',(1.41023353470504E-13,-0.707106781186545,0.70710678118655)) ;
#45743=DIRECTION('center_axis',(1.,-2.73921926332625E-15,-2.02476924116013E-13)) ;
#45744=DIRECTION('ref_axis',(-2.7392192633271E-15,-1.,-4.21482619131383E-15)) ;
#45745=DIRECTION('center_axis',(1.,1.74291365190604E-15,-2.06959057031246E-13)) ;
#45746=DIRECTION('ref_axis',(1.74291365190546E-15,-1.,-2.82240600992864E-15)) ;
#45747=DIRECTION('center_axis',(-2.34486411375479E-15,1.,-2.80866739088387E-15)) ;
#45748=DIRECTION('ref_axis',(-1.79034390112784E-13,0.,-1.)) ;
#45749=DIRECTION('center_axis',(1.,-2.73921926332625E-15,-2.02476924116013E-13)) ;
#45750=DIRECTION('ref_axis',(2.73921926332551E-15,1.,-3.67555483654062E-15)) ;
#45751=DIRECTION('',(2.7392192633255E-15,1.,-3.67555483654062E-15)) ;
#45752=DIRECTION('',(-2.7392192633255E-15,-1.,3.67555483654062E-15)) ;
#45753=DIRECTION('',(2.02476924116013E-13,3.67555483654007E-15,1.)) ;
#45754=DIRECTION('',(2.02476924116013E-13,3.67555483654007E-15,1.)) ;
#45755=DIRECTION('',(2.02476924116013E-13,3.67555483654007E-15,1.)) ;
#45756=DIRECTION('',(2.02476924116013E-13,3.67555483654007E-15,1.)) ;
#45757=DIRECTION('center_axis',(-1.,2.73921926332625E-15,2.02476924116013E-13)) ;
#45758=DIRECTION('ref_axis',(-2.73921926332551E-15,-1.,3.67555483654062E-15)) ;
#45759=DIRECTION('',(2.73921299462249E-15,1.,-3.09600898101992E-8)) ;
#45760=DIRECTION('',(-2.7392192633255E-15,-1.,3.67555483654062E-15)) ;
#45761=DIRECTION('',(-2.02476924116013E-13,-3.67555483654007E-15,-1.)) ;
#45762=DIRECTION('',(-2.02476924116013E-13,-3.67555483654007E-15,-1.)) ;
#45763=DIRECTION('',(-2.02476924116013E-13,-3.67555483654007E-15,-1.)) ;
#45764=DIRECTION('',(-2.02476924116013E-13,-3.67555483654007E-15,-1.)) ;
#45765=DIRECTION('center_axis',(-2.02476924116013E-13,-3.67555483654007E-15,
-1.)) ;
#45766=DIRECTION('ref_axis',(1.,-2.73921926332625E-15,-2.02476924116013E-13)) ;
#45767=DIRECTION('',(-6.86270959829528E-15,1.,7.12661513278716E-15)) ;
#45768=DIRECTION('',(-2.7392192633255E-15,-1.,3.67555483654062E-15)) ;
#45769=DIRECTION('',(1.,-2.73921926332628E-15,-2.11050196179211E-13)) ;
#45770=DIRECTION('',(1.,-2.73921926332624E-15,-1.99601878747771E-13)) ;
#45771=DIRECTION('',(1.,-2.73921926332624E-15,-1.99921328233131E-13)) ;
#45772=DIRECTION('',(1.,-2.73921926332628E-15,-2.10097610394411E-13)) ;
#45773=DIRECTION('center_axis',(2.02476924116013E-13,3.67555483654007E-15,
1.)) ;
#45774=DIRECTION('ref_axis',(-1.,2.73921926332625E-15,2.02476924116013E-13)) ;
#45775=DIRECTION('',(2.7392192633255E-15,1.,-3.67555483654062E-15)) ;
#45776=DIRECTION('',(3.09600846192426E-8,-1.,3.67554856783736E-15)) ;
#45777=DIRECTION('',(-1.,2.73921926332625E-15,2.02476924116013E-13)) ;
#45778=DIRECTION('',(-1.,2.73921926332625E-15,2.02476924116013E-13)) ;
#45779=DIRECTION('',(-1.,2.73921926332626E-15,2.05351969484256E-13)) ;
#45780=DIRECTION('',(-1.,2.73921926332622E-15,1.93903652052816E-13)) ;
#45781=DIRECTION('center_axis',(-2.7392192633255E-15,-1.,3.67555483654062E-15)) ;
#45782=DIRECTION('ref_axis',(-2.02476924116013E-13,-3.67555483654007E-15,
-1.)) ;
#45783=DIRECTION('center_axis',(-7.3207473378131E-15,1.,-1.37355214376752E-14)) ;
#45784=DIRECTION('ref_axis',(0.801573073879436,1.40805385337468E-14,0.597896819887406)) ;
#45785=DIRECTION('center_axis',(3.99202076906257E-14,1.,-4.6659502919908E-14)) ;
#45786=DIRECTION('ref_axis',(-0.597896819887407,6.1269166408667E-14,0.801573073879435)) ;
#45787=DIRECTION('center_axis',(2.7392192633255E-15,1.,-3.67555483654062E-15)) ;
#45788=DIRECTION('ref_axis',(-0.70710679608757,4.53593025184281E-15,0.707106766285525)) ;
#45789=DIRECTION('center_axis',(-1.92665475456957E-15,1.,-9.06964734259742E-15)) ;
#45790=DIRECTION('ref_axis',(-0.801573073879439,-6.96706787756399E-15,-0.597896819887402)) ;
#45791=DIRECTION('center_axis',(-7.32074733780901E-15,1.,6.38441176459794E-15)) ;
#45792=DIRECTION('ref_axis',(0.597896819887408,9.49462411553601E-15,-0.801573073879434)) ;
#45793=DIRECTION('center_axis',(5.67865126919919E-11,-1.,5.65924766963123E-11)) ;
#45794=DIRECTION('ref_axis',(0.728572558446093,2.60902348252204E-12,-0.684968632186405)) ;
#45795=DIRECTION('center_axis',(1.,-2.73921926332625E-15,-2.02476924116013E-13)) ;
#45796=DIRECTION('ref_axis',(2.73921926332551E-15,1.,-3.67555483654062E-15)) ;
#45797=DIRECTION('',(2.73916514353843E-15,0.999999999999964,-2.67288669829288E-7)) ;
#45798=DIRECTION('center_axis',(-2.02476924116013E-13,-3.67555483654007E-15,
-1.)) ;
#45799=DIRECTION('ref_axis',(1.,-2.73921926332625E-15,-2.02476924116013E-13)) ;
#45800=DIRECTION('',(2.67288913307799E-7,-0.999999999999964,3.67550071670292E-15)) ;
#45801=DIRECTION('center_axis',(5.6783473877901E-11,-1.,-5.65819808726216E-11)) ;
#45802=DIRECTION('ref_axis',(-0.684968632186398,2.32918013337625E-12,-0.728572558446099)) ;
#45803=DIRECTION('center_axis',(-1.,2.73921926332625E-15,2.02476924116013E-13)) ;
#45804=DIRECTION('ref_axis',(-2.73921926332551E-15,-1.,3.67555483654062E-15)) ;
#45805=DIRECTION('',(-2.73927338311502E-15,-0.999999999999964,-2.67288675523886E-7)) ;
#45806=DIRECTION('center_axis',(-2.02476924116013E-13,-3.67555483654007E-15,
-1.)) ;
#45807=DIRECTION('ref_axis',(1.,-2.73921926332625E-15,-2.02476924116013E-13)) ;
#45808=DIRECTION('',(-2.67288663414514E-7,0.999999999999964,-3.67550071675352E-15)) ;
#45809=DIRECTION('center_axis',(5.2515080430742E-9,-1.,-5.2515034750072E-9)) ;
#45810=DIRECTION('ref_axis',(-0.728572559766824,-7.42321980239912E-9,0.684968630781598)) ;
#45811=DIRECTION('center_axis',(-5.25072494542696E-9,-1.,5.25067969529154E-9)) ;
#45812=DIRECTION('ref_axis',(-0.707106793325164,7.42561443343648E-9,0.707106769047931)) ;
#45813=DIRECTION('center_axis',(-1.,2.73921926332625E-15,2.02476924116013E-13)) ;
#45814=DIRECTION('ref_axis',(-2.73921926332551E-15,-1.,3.67555483654062E-15)) ;
#45815=DIRECTION('',(2.7392965773295E-15,0.999999999999927,3.81841060590217E-7)) ;
#45816=DIRECTION('center_axis',(2.02476924116013E-13,3.67555483654007E-15,
1.)) ;
#45817=DIRECTION('ref_axis',(-1.,2.73921926332625E-15,2.02476924116013E-13)) ;
#45818=DIRECTION('',(-3.81841078221714E-7,-0.999999999999927,3.67563215054682E-15)) ;
#45819=DIRECTION('center_axis',(-5.64897426180912E-11,-1.,5.68916334461304E-11)) ;
#45820=DIRECTION('ref_axis',(0.684968632186416,2.75598120034729E-12,0.728572558446082)) ;
#45821=DIRECTION('center_axis',(1.,-2.73921926332625E-15,-2.02476924116013E-13)) ;
#45822=DIRECTION('ref_axis',(2.73921926332551E-15,1.,-3.67555483654062E-15)) ;
#45823=DIRECTION('',(-2.73916514353579E-15,-0.999999999999964,2.67288682874995E-7)) ;
#45824=DIRECTION('center_axis',(2.02476924116013E-13,3.67555483654007E-15,
1.)) ;
#45825=DIRECTION('ref_axis',(-1.,2.73921926332625E-15,2.02476924116013E-13)) ;
#45826=DIRECTION('',(2.67288668892953E-7,0.999999999999964,-3.67560895632747E-15)) ;
#45827=DIRECTION('center_axis',(-2.7392192633255E-15,-1.,3.67555483654062E-15)) ;
#45828=DIRECTION('ref_axis',(-0.707106792894461,4.53593025483263E-15,0.707106769478634)) ;
#45829=DIRECTION('center_axis',(-2.7392192633255E-15,-1.,3.67555483654062E-15)) ;
#45830=DIRECTION('ref_axis',(0.707106781816028,-4.53593026520576E-15,-0.707106780557067)) ;
#45831=DIRECTION('center_axis',(-2.7392192633255E-15,-1.,3.67555483654062E-15)) ;
#45832=DIRECTION('ref_axis',(-0.707106792894461,4.53593025483263E-15,0.707106769478634)) ;
#45833=DIRECTION('center_axis',(-2.7392192633255E-15,-1.,3.67555483654062E-15)) ;
#45834=DIRECTION('ref_axis',(-0.707106792894461,4.53593025483263E-15,0.707106769478634)) ;
#80803=CARTESIAN_POINT('',(0.,0.,0.)) ;
#80804=CARTESIAN_POINT('Ctrl Pts',(127.032036789131,-75.3686363338475,-197.090005390471)) ;
#80805=CARTESIAN_POINT('Ctrl Pts',(123.222036869419,-75.3686363338475,-200.90000547076)) ;
#80806=CARTESIAN_POINT('Ctrl Pts',(127.032036949709,-75.3686363338475,-204.710005390471)) ;
#80807=CARTESIAN_POINT('Ctrl Pts',(130.842037029998,-75.3686363338475,-208.520005310182)) ;
#80808=CARTESIAN_POINT('Ctrl Pts',(134.652036949709,-75.3686363338475,-204.710005229893)) ;
#80809=CARTESIAN_POINT('Ctrl Pts',(138.46203686942,-75.3686363338475,-200.900005149604)) ;
#80810=CARTESIAN_POINT('Ctrl Pts',(134.652036789131,-75.3686363338475,-197.090005229893)) ;
#80811=CARTESIAN_POINT('Ctrl Pts',(130.842036708842,-75.3686363338475,-193.280005310182)) ;
#80812=CARTESIAN_POINT('Ctrl Pts',(127.032036789131,-75.3686363338475,-197.090005390471)) ;
#80813=CARTESIAN_POINT('Ctrl Pts',(127.032036789131,-75.1781363338475,-197.090005390471)) ;
#80814=CARTESIAN_POINT('Ctrl Pts',(123.222036869419,-75.1781363338475,-200.90000547076)) ;
#80815=CARTESIAN_POINT('Ctrl Pts',(127.032036949709,-75.1781363338475,-204.710005390471)) ;
#80816=CARTESIAN_POINT('Ctrl Pts',(130.842037029998,-75.1781363338475,-208.520005310182)) ;
#80817=CARTESIAN_POINT('Ctrl Pts',(134.652036949709,-75.1781363338475,-204.710005229893)) ;
#80818=CARTESIAN_POINT('Ctrl Pts',(138.46203686942,-75.1781363338475,-200.900005149604)) ;
#80819=CARTESIAN_POINT('Ctrl Pts',(134.652036789131,-75.1781363338475,-197.090005229893)) ;
#80820=CARTESIAN_POINT('Ctrl Pts',(130.842036708842,-75.1781363338475,-193.280005310182)) ;
#80821=CARTESIAN_POINT('Ctrl Pts',(127.032036789131,-75.1781363338475,-197.090005390471)) ;
#80822=CARTESIAN_POINT('Ctrl Pts',(127.481049604646,-75.1781363338475,-197.539018187062)) ;
#80823=CARTESIAN_POINT('Ctrl Pts',(124.120062481526,-75.1781363338475,-200.900005451836)) ;
#80824=CARTESIAN_POINT('Ctrl Pts',(127.4810497463,-75.1781363338475,-204.260992574956)) ;
#80825=CARTESIAN_POINT('Ctrl Pts',(130.842037011073,-75.1781363338475,-207.621979698075)) ;
#80826=CARTESIAN_POINT('Ctrl Pts',(134.203024134193,-75.1781363338475,-204.260992433302)) ;
#80827=CARTESIAN_POINT('Ctrl Pts',(137.564011257313,-75.1781363338475,-200.900005168529)) ;
#80828=CARTESIAN_POINT('Ctrl Pts',(134.203023992539,-75.1781363338475,-197.539018045409)) ;
#80829=CARTESIAN_POINT('Ctrl Pts',(130.842036727766,-75.1781363338475,-194.178030922289)) ;
#80830=CARTESIAN_POINT('Ctrl Pts',(127.481049604646,-75.1781363338475,-197.539018187062)) ;
#80831=CARTESIAN_POINT('',(128.000141404111,-75.1781363338475,-197.090005310182)) ;
#80832=CARTESIAN_POINT('',(127.260059362794,-75.2257613351713,-197.09000531248)) ;
#80833=CARTESIAN_POINT('Ctrl Pts',(128.000141404111,-75.1781363338475,-197.090005310182)) ;
#80834=CARTESIAN_POINT('Ctrl Pts',(127.875189846825,-75.1781363338475,-197.090005310182)) ;
#80835=CARTESIAN_POINT('Ctrl Pts',(127.74042967657,-75.1801139619557,-197.090005310065)) ;
#80836=CARTESIAN_POINT('Ctrl Pts',(127.489185117998,-75.1931618999273,-197.090005310065)) ;
#80837=CARTESIAN_POINT('Ctrl Pts',(127.362906128424,-75.2046272926173,-197.090005310182)) ;
#80838=CARTESIAN_POINT('Ctrl Pts',(127.260059363022,-75.2257613362829,-197.090005310182)) ;
#80839=CARTESIAN_POINT('',(127.481049604646,-75.1781363338475,-197.539018187062)) ;
#80840=CARTESIAN_POINT('Origin',(130.842036869419,-75.1781363338481,-200.900005310182)) ;
#80841=CARTESIAN_POINT('',(127.144290007455,-75.2257613338475,-197.202258575173)) ;
#80842=CARTESIAN_POINT('Ctrl Pts',(127.144290007455,-75.2257613338475,-197.202258575173)) ;
#80843=CARTESIAN_POINT('Ctrl Pts',(127.2191254716,-75.1940113338475,-197.277094046379)) ;
#80844=CARTESIAN_POINT('Ctrl Pts',(127.331378670518,-75.1781363338475,-197.389347250489)) ;
#80845=CARTESIAN_POINT('Ctrl Pts',(127.481049604646,-75.1781363338475,-197.539018187062)) ;
#80846=CARTESIAN_POINT('Origin',(130.842036960968,-75.225761372682,-200.90000540173)) ;
#80847=CARTESIAN_POINT('Ctrl Pts',(127.032036789131,-75.3686363338475,-197.090005390471)) ;
#80848=CARTESIAN_POINT('Ctrl Pts',(123.222036869419,-75.3686363338475,-200.90000547076)) ;
#80849=CARTESIAN_POINT('Ctrl Pts',(127.032036949709,-75.3686363338475,-204.710005390471)) ;
#80850=CARTESIAN_POINT('Ctrl Pts',(130.842037029998,-75.3686363338475,-208.520005310182)) ;
#80851=CARTESIAN_POINT('Ctrl Pts',(134.652036949709,-75.3686363338475,-204.710005229893)) ;
#80852=CARTESIAN_POINT('Ctrl Pts',(138.46203686942,-75.3686363338475,-200.900005149604)) ;
#80853=CARTESIAN_POINT('Ctrl Pts',(134.652036789131,-75.3686363338475,-197.090005229893)) ;
#80854=CARTESIAN_POINT('Ctrl Pts',(130.842036708842,-75.3686363338475,-193.280005310182)) ;
#80855=CARTESIAN_POINT('Ctrl Pts',(127.032036789131,-75.3686363338475,-197.090005390471)) ;
#80856=CARTESIAN_POINT('Ctrl Pts',(127.032036789131,-75.1781363338475,-197.090005390471)) ;
#80857=CARTESIAN_POINT('Ctrl Pts',(123.222036869419,-75.1781363338475,-200.90000547076)) ;
#80858=CARTESIAN_POINT('Ctrl Pts',(127.032036949709,-75.1781363338475,-204.710005390471)) ;
#80859=CARTESIAN_POINT('Ctrl Pts',(130.842037029998,-75.1781363338475,-208.520005310182)) ;
#80860=CARTESIAN_POINT('Ctrl Pts',(134.652036949709,-75.1781363338475,-204.710005229893)) ;
#80861=CARTESIAN_POINT('Ctrl Pts',(138.46203686942,-75.1781363338475,-200.900005149604)) ;
#80862=CARTESIAN_POINT('Ctrl Pts',(134.652036789131,-75.1781363338475,-197.090005229893)) ;
#80863=CARTESIAN_POINT('Ctrl Pts',(130.842036708842,-75.1781363338475,-193.280005310182)) ;
#80864=CARTESIAN_POINT('Ctrl Pts',(127.032036789131,-75.1781363338475,-197.090005390471)) ;
#80865=CARTESIAN_POINT('Ctrl Pts',(127.481049604646,-75.1781363338475,-197.539018187062)) ;
#80866=CARTESIAN_POINT('Ctrl Pts',(124.120062481526,-75.1781363338475,-200.900005451836)) ;
#80867=CARTESIAN_POINT('Ctrl Pts',(127.4810497463,-75.1781363338475,-204.260992574956)) ;
#80868=CARTESIAN_POINT('Ctrl Pts',(130.842037011073,-75.1781363338475,-207.621979698075)) ;
#80869=CARTESIAN_POINT('Ctrl Pts',(134.203024134193,-75.1781363338475,-204.260992433302)) ;
#80870=CARTESIAN_POINT('Ctrl Pts',(137.564011257313,-75.1781363338475,-200.900005168529)) ;
#80871=CARTESIAN_POINT('Ctrl Pts',(134.203023992539,-75.1781363338475,-197.539018045409)) ;
#80872=CARTESIAN_POINT('Ctrl Pts',(130.842036727766,-75.1781363338475,-194.178030922289)) ;
#80873=CARTESIAN_POINT('Ctrl Pts',(127.481049604646,-75.1781363338475,-197.539018187062)) ;
#80874=CARTESIAN_POINT('',(133.683932334728,-75.1781363338475,-204.710005310183)) ;
#80875=CARTESIAN_POINT('',(134.424014363965,-75.2257613338475,-204.710005310183)) ;
#80876=CARTESIAN_POINT('Ctrl Pts',(133.683932334728,-75.1781363338475,-204.710005310182)) ;
#80877=CARTESIAN_POINT('Ctrl Pts',(133.808883889989,-75.1781363338475,-204.710005310182)) ;
#80878=CARTESIAN_POINT('Ctrl Pts',(133.943644057601,-75.1801139618916,-204.710005310299)) ;
#80879=CARTESIAN_POINT('Ctrl Pts',(134.194892600511,-75.193162106426,-204.710005310299)) ;
#80880=CARTESIAN_POINT('Ctrl Pts',(134.321165640767,-75.2046268889911,-204.710005310182)) ;
#80881=CARTESIAN_POINT('Ctrl Pts',(134.424014363965,-75.2257613338474,-204.710005310183)) ;
#80882=CARTESIAN_POINT('',(134.652036869419,-75.1781363338475,-203.741900775492)) ;
#80883=CARTESIAN_POINT('Origin',(130.84203686942,-75.1781363338476,-200.900005310182)) ;
#80884=CARTESIAN_POINT('',(134.652036869419,-75.2257613338475,-204.481982804729)) ;
#80885=CARTESIAN_POINT('Ctrl Pts',(134.652036869419,-75.2257613338474,-204.481982804729)) ;
#80886=CARTESIAN_POINT('Ctrl Pts',(134.652036869419,-75.2046268889901,-204.379134081526)) ;
#80887=CARTESIAN_POINT('Ctrl Pts',(134.652036869535,-75.1931621064255,-204.252861041264)) ;
#80888=CARTESIAN_POINT('Ctrl Pts',(134.652036869535,-75.1801139618916,-204.001612498367)) ;
#80889=CARTESIAN_POINT('Ctrl Pts',(134.652036869419,-75.1781363338475,-203.866852330753)) ;
#80890=CARTESIAN_POINT('Ctrl Pts',(134.652036869419,-75.1781363338475,-203.741900775492)) ;
#80891=CARTESIAN_POINT('Origin',(130.842036869419,-75.225761333849,-200.900005310182)) ;
#80892=CARTESIAN_POINT('Ctrl Pts',(127.032036789131,-75.3686363338475,-197.090005390471)) ;
#80893=CARTESIAN_POINT('Ctrl Pts',(123.222036869419,-75.3686363338475,-200.90000547076)) ;
#80894=CARTESIAN_POINT('Ctrl Pts',(127.032036949709,-75.3686363338475,-204.710005390471)) ;
#80895=CARTESIAN_POINT('Ctrl Pts',(130.842037029998,-75.3686363338475,-208.520005310182)) ;
#80896=CARTESIAN_POINT('Ctrl Pts',(134.652036949709,-75.3686363338475,-204.710005229893)) ;
#80897=CARTESIAN_POINT('Ctrl Pts',(138.46203686942,-75.3686363338475,-200.900005149604)) ;
#80898=CARTESIAN_POINT('Ctrl Pts',(134.652036789131,-75.3686363338475,-197.090005229893)) ;
#80899=CARTESIAN_POINT('Ctrl Pts',(130.842036708842,-75.3686363338475,-193.280005310182)) ;
#80900=CARTESIAN_POINT('Ctrl Pts',(127.032036789131,-75.3686363338475,-197.090005390471)) ;
#80901=CARTESIAN_POINT('Ctrl Pts',(127.032036789131,-75.1781363338475,-197.090005390471)) ;
#80902=CARTESIAN_POINT('Ctrl Pts',(123.222036869419,-75.1781363338475,-200.90000547076)) ;
#80903=CARTESIAN_POINT('Ctrl Pts',(127.032036949709,-75.1781363338475,-204.710005390471)) ;
#80904=CARTESIAN_POINT('Ctrl Pts',(130.842037029998,-75.1781363338475,-208.520005310182)) ;
#80905=CARTESIAN_POINT('Ctrl Pts',(134.652036949709,-75.1781363338475,-204.710005229893)) ;
#80906=CARTESIAN_POINT('Ctrl Pts',(138.46203686942,-75.1781363338475,-200.900005149604)) ;
#80907=CARTESIAN_POINT('Ctrl Pts',(134.652036789131,-75.1781363338475,-197.090005229893)) ;
#80908=CARTESIAN_POINT('Ctrl Pts',(130.842036708842,-75.1781363338475,-193.280005310182)) ;
#80909=CARTESIAN_POINT('Ctrl Pts',(127.032036789131,-75.1781363338475,-197.090005390471)) ;
#80910=CARTESIAN_POINT('Ctrl Pts',(127.481049604646,-75.1781363338475,-197.539018187062)) ;
#80911=CARTESIAN_POINT('Ctrl Pts',(124.120062481526,-75.1781363338475,-200.900005451836)) ;
#80912=CARTESIAN_POINT('Ctrl Pts',(127.4810497463,-75.1781363338475,-204.260992574956)) ;
#80913=CARTESIAN_POINT('Ctrl Pts',(130.842037011073,-75.1781363338475,-207.621979698075)) ;
#80914=CARTESIAN_POINT('Ctrl Pts',(134.203024134193,-75.1781363338475,-204.260992433302)) ;
#80915=CARTESIAN_POINT('Ctrl Pts',(137.564011257313,-75.1781363338475,-200.900005168529)) ;
#80916=CARTESIAN_POINT('Ctrl Pts',(134.203023992539,-75.1781363338475,-197.539018045409)) ;
#80917=CARTESIAN_POINT('Ctrl Pts',(130.842036727766,-75.1781363338475,-194.178030922289)) ;
#80918=CARTESIAN_POINT('Ctrl Pts',(127.481049604646,-75.1781363338475,-197.539018187062)) ;
#80919=CARTESIAN_POINT('',(127.03203686942,-75.1781363338475,-198.058109844872)) ;
#80920=CARTESIAN_POINT('Origin',(130.84203686942,-75.1781363338475,-200.900005310182)) ;
#80921=CARTESIAN_POINT('',(127.032036867121,-75.2257613325238,-197.318027827716)) ;
#80922=CARTESIAN_POINT('Ctrl Pts',(127.03203686942,-75.2257613314121,-197.318027827487)) ;
#80923=CARTESIAN_POINT('Ctrl Pts',(127.03203686942,-75.2046272023282,-197.420875019449)) ;
#80924=CARTESIAN_POINT('Ctrl Pts',(127.032036869317,-75.1931624628046,-197.547145758675)) ;
#80925=CARTESIAN_POINT('Ctrl Pts',(127.032036869317,-75.1801140186575,-197.798393987226)) ;
#80926=CARTESIAN_POINT('Ctrl Pts',(127.03203686942,-75.1781363338475,-197.933156496317)) ;
#80927=CARTESIAN_POINT('Ctrl Pts',(127.03203686942,-75.1781363338475,-198.058109844872)) ;
#80928=CARTESIAN_POINT('Origin',(130.842036777871,-75.225761295013,-200.900005218634)) ;
#80929=CARTESIAN_POINT('Ctrl Pts',(127.032036789131,-75.3686363338475,-197.090005390471)) ;
#80930=CARTESIAN_POINT('Ctrl Pts',(123.222036869419,-75.3686363338475,-200.90000547076)) ;
#80931=CARTESIAN_POINT('Ctrl Pts',(127.032036949709,-75.3686363338475,-204.710005390471)) ;
#80932=CARTESIAN_POINT('Ctrl Pts',(130.842037029998,-75.3686363338475,-208.520005310182)) ;
#80933=CARTESIAN_POINT('Ctrl Pts',(134.652036949709,-75.3686363338475,-204.710005229893)) ;
#80934=CARTESIAN_POINT('Ctrl Pts',(138.46203686942,-75.3686363338475,-200.900005149604)) ;
#80935=CARTESIAN_POINT('Ctrl Pts',(134.652036789131,-75.3686363338475,-197.090005229893)) ;
#80936=CARTESIAN_POINT('Ctrl Pts',(130.842036708842,-75.3686363338475,-193.280005310182)) ;
#80937=CARTESIAN_POINT('Ctrl Pts',(127.032036789131,-75.3686363338475,-197.090005390471)) ;
#80938=CARTESIAN_POINT('Ctrl Pts',(127.032036789131,-75.1781363338475,-197.090005390471)) ;
#80939=CARTESIAN_POINT('Ctrl Pts',(123.222036869419,-75.1781363338475,-200.90000547076)) ;
#80940=CARTESIAN_POINT('Ctrl Pts',(127.032036949709,-75.1781363338475,-204.710005390471)) ;
#80941=CARTESIAN_POINT('Ctrl Pts',(130.842037029998,-75.1781363338475,-208.520005310182)) ;
#80942=CARTESIAN_POINT('Ctrl Pts',(134.652036949709,-75.1781363338475,-204.710005229893)) ;
#80943=CARTESIAN_POINT('Ctrl Pts',(138.46203686942,-75.1781363338475,-200.900005149604)) ;
#80944=CARTESIAN_POINT('Ctrl Pts',(134.652036789131,-75.1781363338475,-197.090005229893)) ;
#80945=CARTESIAN_POINT('Ctrl Pts',(130.842036708842,-75.1781363338475,-193.280005310182)) ;
#80946=CARTESIAN_POINT('Ctrl Pts',(127.032036789131,-75.1781363338475,-197.090005390471)) ;
#80947=CARTESIAN_POINT('Ctrl Pts',(127.481049604646,-75.1781363338475,-197.539018187062)) ;
#80948=CARTESIAN_POINT('Ctrl Pts',(124.120062481526,-75.1781363338475,-200.900005451836)) ;
#80949=CARTESIAN_POINT('Ctrl Pts',(127.4810497463,-75.1781363338475,-204.260992574956)) ;
#80950=CARTESIAN_POINT('Ctrl Pts',(130.842037011073,-75.1781363338475,-207.621979698075)) ;
#80951=CARTESIAN_POINT('Ctrl Pts',(134.203024134193,-75.1781363338475,-204.260992433302)) ;
#80952=CARTESIAN_POINT('Ctrl Pts',(137.564011257313,-75.1781363338475,-200.900005168529)) ;
#80953=CARTESIAN_POINT('Ctrl Pts',(134.203023992539,-75.1781363338475,-197.539018045409)) ;
#80954=CARTESIAN_POINT('Ctrl Pts',(130.842036727766,-75.1781363338475,-194.178030922289)) ;
#80955=CARTESIAN_POINT('Ctrl Pts',(127.481049604646,-75.1781363338475,-197.539018187062)) ;
#80956=CARTESIAN_POINT('',(127.032036869419,-75.1781363338475,-203.741900775491)) ;
#80957=CARTESIAN_POINT('',(127.032036869419,-75.2257613338475,-204.481982804728)) ;
#80958=CARTESIAN_POINT('Ctrl Pts',(127.032036869419,-75.1781363338475,-203.741900775491)) ;
#80959=CARTESIAN_POINT('Ctrl Pts',(127.032036869419,-75.1781363338475,-203.866852330753)) ;
#80960=CARTESIAN_POINT('Ctrl Pts',(127.032036869302,-75.1801139618916,-204.001612498365)) ;
#80961=CARTESIAN_POINT('Ctrl Pts',(127.032036869302,-75.1931618993063,-204.252857053077)) ;
#80962=CARTESIAN_POINT('Ctrl Pts',(127.032036869419,-75.2046272914575,-204.379136040093)) ;
#80963=CARTESIAN_POINT('Ctrl Pts',(127.032036869418,-75.2257613338477,-204.481982804728)) ;
#80964=CARTESIAN_POINT('',(128.000141404109,-75.1781363338475,-204.710005310182)) ;
#80965=CARTESIAN_POINT('Origin',(130.84203686942,-75.1781363338476,-200.900005310182)) ;
#80966=CARTESIAN_POINT('',(127.260059374872,-75.2257613338475,-204.710005310181)) ;
#80967=CARTESIAN_POINT('Ctrl Pts',(127.260059374872,-75.2257613338476,-204.710005310181)) ;
#80968=CARTESIAN_POINT('Ctrl Pts',(127.362904608918,-75.204627605979,-204.710005310181)) ;
#80969=CARTESIAN_POINT('Ctrl Pts',(127.489181296476,-75.1931622563878,-204.710005310284)) ;
#80970=CARTESIAN_POINT('Ctrl Pts',(127.740425541024,-75.1801140187322,-204.710005310284)) ;
#80971=CARTESIAN_POINT('Ctrl Pts',(127.875188053195,-75.1781363338475,-204.710005310181)) ;
#80972=CARTESIAN_POINT('Ctrl Pts',(128.000141404109,-75.1781363338475,-204.710005310181)) ;
#80973=CARTESIAN_POINT('Origin',(130.842036869419,-75.2257613338505,-200.900005310183)) ;
#80974=CARTESIAN_POINT('Ctrl Pts',(127.032036789131,-75.3686363338475,-197.090005390471)) ;
#80975=CARTESIAN_POINT('Ctrl Pts',(123.222036869419,-75.3686363338475,-200.90000547076)) ;
#80976=CARTESIAN_POINT('Ctrl Pts',(127.032036949709,-75.3686363338475,-204.710005390471)) ;
#80977=CARTESIAN_POINT('Ctrl Pts',(130.842037029998,-75.3686363338475,-208.520005310182)) ;
#80978=CARTESIAN_POINT('Ctrl Pts',(134.652036949709,-75.3686363338475,-204.710005229893)) ;
#80979=CARTESIAN_POINT('Ctrl Pts',(138.46203686942,-75.3686363338475,-200.900005149604)) ;
#80980=CARTESIAN_POINT('Ctrl Pts',(134.652036789131,-75.3686363338475,-197.090005229893)) ;
#80981=CARTESIAN_POINT('Ctrl Pts',(130.842036708842,-75.3686363338475,-193.280005310182)) ;
#80982=CARTESIAN_POINT('Ctrl Pts',(127.032036789131,-75.3686363338475,-197.090005390471)) ;
#80983=CARTESIAN_POINT('Ctrl Pts',(127.032036789131,-75.1781363338475,-197.090005390471)) ;
#80984=CARTESIAN_POINT('Ctrl Pts',(123.222036869419,-75.1781363338475,-200.90000547076)) ;
#80985=CARTESIAN_POINT('Ctrl Pts',(127.032036949709,-75.1781363338475,-204.710005390471)) ;
#80986=CARTESIAN_POINT('Ctrl Pts',(130.842037029998,-75.1781363338475,-208.520005310182)) ;
#80987=CARTESIAN_POINT('Ctrl Pts',(134.652036949709,-75.1781363338475,-204.710005229893)) ;
#80988=CARTESIAN_POINT('Ctrl Pts',(138.46203686942,-75.1781363338475,-200.900005149604)) ;
#80989=CARTESIAN_POINT('Ctrl Pts',(134.652036789131,-75.1781363338475,-197.090005229893)) ;
#80990=CARTESIAN_POINT('Ctrl Pts',(130.842036708842,-75.1781363338475,-193.280005310182)) ;
#80991=CARTESIAN_POINT('Ctrl Pts',(127.032036789131,-75.1781363338475,-197.090005390471)) ;
#80992=CARTESIAN_POINT('Ctrl Pts',(127.481049604646,-75.1781363338475,-197.539018187062)) ;
#80993=CARTESIAN_POINT('Ctrl Pts',(124.120062481526,-75.1781363338475,-200.900005451836)) ;
#80994=CARTESIAN_POINT('Ctrl Pts',(127.4810497463,-75.1781363338475,-204.260992574956)) ;
#80995=CARTESIAN_POINT('Ctrl Pts',(130.842037011073,-75.1781363338475,-207.621979698075)) ;
#80996=CARTESIAN_POINT('Ctrl Pts',(134.203024134193,-75.1781363338475,-204.260992433302)) ;
#80997=CARTESIAN_POINT('Ctrl Pts',(137.564011257313,-75.1781363338475,-200.900005168529)) ;
#80998=CARTESIAN_POINT('Ctrl Pts',(134.203023992539,-75.1781363338475,-197.539018045409)) ;
#80999=CARTESIAN_POINT('Ctrl Pts',(130.842036727766,-75.1781363338475,-194.178030922289)) ;
#81000=CARTESIAN_POINT('Ctrl Pts',(127.481049604646,-75.1781363338475,-197.539018187062)) ;
#81001=CARTESIAN_POINT('',(134.65203686942,-75.1781363338475,-198.058109844874)) ;
#81002=CARTESIAN_POINT('',(134.65203686942,-75.2257613338475,-197.318027815637)) ;
#81003=CARTESIAN_POINT('Ctrl Pts',(134.65203686942,-75.1781363338475,-198.058109844874)) ;
#81004=CARTESIAN_POINT('Ctrl Pts',(134.65203686942,-75.1781363338475,-197.93315649396)) ;
#81005=CARTESIAN_POINT('Ctrl Pts',(134.652036869524,-75.1801140187322,-197.798393981794)) ;
#81006=CARTESIAN_POINT('Ctrl Pts',(134.652036869524,-75.193162256388,-197.547149737234)) ;
#81007=CARTESIAN_POINT('Ctrl Pts',(134.65203686942,-75.2046276059798,-197.420873049679)) ;
#81008=CARTESIAN_POINT('Ctrl Pts',(134.65203686942,-75.2257613338474,-197.318027815637)) ;
#81009=CARTESIAN_POINT('',(133.683932334729,-75.1781363338475,-197.090005310183)) ;
#81010=CARTESIAN_POINT('Origin',(130.84203686942,-75.1781363338475,-200.900005310182)) ;
#81011=CARTESIAN_POINT('',(134.424014363967,-75.2257613338475,-197.090005310183)) ;
#81012=CARTESIAN_POINT('Ctrl Pts',(134.424014363967,-75.2257613338475,-197.090005310183)) ;
#81013=CARTESIAN_POINT('Ctrl Pts',(134.321167599324,-75.2046272914557,-197.090005310183)) ;
#81014=CARTESIAN_POINT('Ctrl Pts',(134.194888612299,-75.1931618993052,-197.090005310067)) ;
#81015=CARTESIAN_POINT('Ctrl Pts',(133.943644057601,-75.1801139618915,-197.090005310067)) ;
#81016=CARTESIAN_POINT('Ctrl Pts',(133.808883889988,-75.1781363338475,-197.090005310183)) ;
#81017=CARTESIAN_POINT('Ctrl Pts',(133.683932334729,-75.1781363338475,-197.090005310183)) ;
#81018=CARTESIAN_POINT('Origin',(130.842036869419,-75.2257613338461,-200.900005310183)) ;
#81019=CARTESIAN_POINT('Origin',(130.84203686942,-75.4956363338475,-200.900005310182)) ;
#81020=CARTESIAN_POINT('',(130.84203686942,-75.1781363338475,-199.249005310182)) ;
#81021=CARTESIAN_POINT('Origin',(130.84203686942,-75.1781363338475,-200.900005310182)) ;
#81022=CARTESIAN_POINT('',(130.84203686942,-75.8131363338475,-199.249005310182)) ;
#81023=CARTESIAN_POINT('',(130.84203686942,-75.4956363338475,-199.249005310182)) ;
#81024=CARTESIAN_POINT('Origin',(130.84203686942,-75.8131363338475,-200.900005310182)) ;
#81025=CARTESIAN_POINT('Origin',(134.65203686942,-75.1781363338475,-197.090005310183)) ;
#81026=CARTESIAN_POINT('',(131.572286869419,-75.1781363338475,-204.710005310182)) ;
#81027=CARTESIAN_POINT('',(131.572286869419,-75.1781363338475,-204.710005310182)) ;
#81028=CARTESIAN_POINT('',(131.572286870962,-75.1781363338475,-203.440005310188)) ;
#81029=CARTESIAN_POINT('',(131.572286869419,-75.1781363338475,-204.710005310182)) ;
#81030=CARTESIAN_POINT('',(130.111786868562,-75.1781363338475,-203.440005310187)) ;
#81031=CARTESIAN_POINT('Origin',(130.84203687019,-75.1781363338475,-203.440005310182)) ;
#81032=CARTESIAN_POINT('',(130.111786869419,-75.1781363338475,-204.710005310182)) ;
#81033=CARTESIAN_POINT('',(130.111786869419,-75.1781363338475,-203.440005310187)) ;
#81034=CARTESIAN_POINT('',(128.000141404109,-75.1781363338475,-204.710005310182)) ;
#81035=CARTESIAN_POINT('',(127.032036869419,-75.1781363338475,-201.630255310181)) ;
#81036=CARTESIAN_POINT('',(127.032036869419,-75.1781363338475,-201.630255310181)) ;
#81037=CARTESIAN_POINT('',(128.302036869413,-75.1781363338475,-201.630255311724)) ;
#81038=CARTESIAN_POINT('',(127.032036869419,-75.1781363338475,-201.630255310181)) ;
#81039=CARTESIAN_POINT('',(128.302036869415,-75.1781363338475,-200.169755309325)) ;
#81040=CARTESIAN_POINT('Origin',(128.30203686942,-75.1781363338475,-200.900005310953)) ;
#81041=CARTESIAN_POINT('',(127.03203686942,-75.1781363338475,-200.169755310181)) ;
#81042=CARTESIAN_POINT('',(128.302036869415,-75.1781363338475,-200.169755310182)) ;
#81043=CARTESIAN_POINT('',(127.03203686942,-75.1781363338475,-198.058109844872)) ;
#81044=CARTESIAN_POINT('',(130.11178686942,-75.1781363338475,-197.090005310182)) ;
#81045=CARTESIAN_POINT('',(130.11178686942,-75.1781363338475,-197.090005310182)) ;
#81046=CARTESIAN_POINT('',(130.111786867877,-75.1781363338475,-198.360005310176)) ;
#81047=CARTESIAN_POINT('',(130.11178686942,-75.1781363338475,-197.090005310182)) ;
#81048=CARTESIAN_POINT('',(131.572286870277,-75.1781363338475,-198.360005310177)) ;
#81049=CARTESIAN_POINT('Origin',(130.842036868649,-75.1781363338475,-198.360005310182)) ;
#81050=CARTESIAN_POINT('',(131.57228686942,-75.1781363338475,-197.090005310182)) ;
#81051=CARTESIAN_POINT('',(131.57228686942,-75.1781363338475,-198.360005310177)) ;
#81052=CARTESIAN_POINT('',(133.683932334729,-75.1781363338475,-197.090005310183)) ;
#81053=CARTESIAN_POINT('',(134.65203686942,-75.1781363338475,-200.169755310183)) ;
#81054=CARTESIAN_POINT('',(134.65203686942,-75.1781363338475,-200.169755310183)) ;
#81055=CARTESIAN_POINT('',(133.382036869426,-75.1781363338475,-200.16975530864)) ;
#81056=CARTESIAN_POINT('',(134.65203686942,-75.1781363338475,-200.169755310183)) ;
#81057=CARTESIAN_POINT('',(133.382036869424,-75.1781363338475,-201.63025531104)) ;
#81058=CARTESIAN_POINT('Origin',(133.38203686942,-75.1781363338475,-200.900005309411)) ;
#81059=CARTESIAN_POINT('',(134.652036869419,-75.1781363338475,-201.630255310183)) ;
#81060=CARTESIAN_POINT('',(133.382036869424,-75.1781363338475,-201.630255310183)) ;
#81061=CARTESIAN_POINT('',(134.652036869419,-75.1781363338475,-203.741900775492)) ;
#81062=CARTESIAN_POINT('Origin',(134.890161869419,-75.3686363338475,-201.693755310183)) ;
#81063=CARTESIAN_POINT('',(134.65203686942,-75.3686363338475,-200.328505310183)) ;
#81064=CARTESIAN_POINT('',(133.382036869411,-75.3686363338475,-200.328505308646)) ;
#81065=CARTESIAN_POINT('',(134.65203686942,-75.3686363338475,-200.328505310183)) ;
#81066=CARTESIAN_POINT('',(134.652036869419,-75.3686363338475,-201.471505310183)) ;
#81067=CARTESIAN_POINT('',(134.652036869419,-75.3686363338475,-201.471505310183)) ;
#81068=CARTESIAN_POINT('',(133.382036869422,-75.3686363338475,-201.471505311719)) ;
#81069=CARTESIAN_POINT('',(133.382036869422,-75.3686363338475,-201.471505311335)) ;
#81070=CARTESIAN_POINT('Origin',(133.38203686942,-75.3686363338475,-200.900005310183)) ;
#81071=CARTESIAN_POINT('Origin',(126.79391186942,-75.3686363338475,-200.106255310181)) ;
#81072=CARTESIAN_POINT('',(127.03203686942,-75.3686363338475,-200.328505310181)) ;
#81073=CARTESIAN_POINT('',(127.032036869419,-75.3686363338475,-201.471505310181)) ;
#81074=CARTESIAN_POINT('',(127.03203686942,-75.3686363338475,-200.328505310181)) ;
#81075=CARTESIAN_POINT('',(128.302036869418,-75.3686363338475,-200.328505308645)) ;
#81076=CARTESIAN_POINT('',(128.302036869418,-75.3686363338475,-200.328505309029)) ;
#81077=CARTESIAN_POINT('',(128.30203686943,-75.3686363338475,-201.471505311718)) ;
#81078=CARTESIAN_POINT('Origin',(128.30203686942,-75.3686363338475,-200.900005310182)) ;
#81079=CARTESIAN_POINT('',(127.032036869419,-75.3686363338475,-201.471505310181)) ;
#81080=CARTESIAN_POINT('Origin',(130.048286869419,-75.3686363338475,-204.948130310182)) ;
#81081=CARTESIAN_POINT('',(131.413536869419,-75.3686363338475,-204.710005310182)) ;
#81082=CARTESIAN_POINT('',(131.413536870956,-75.3686363338475,-203.440005310174)) ;
#81083=CARTESIAN_POINT('',(131.413536869419,-75.3686363338475,-204.710005310182)) ;
#81084=CARTESIAN_POINT('',(130.270536869419,-75.3686363338475,-204.710005310182)) ;
#81085=CARTESIAN_POINT('',(130.270536869419,-75.3686363338475,-204.710005310182)) ;
#81086=CARTESIAN_POINT('',(130.270536867882,-75.3686363338475,-203.440005310184)) ;
#81087=CARTESIAN_POINT('',(130.270536868267,-75.3686363338475,-203.440005310184)) ;
#81088=CARTESIAN_POINT('Origin',(130.842036869419,-75.3686363338475,-203.440005310182)) ;
#81089=CARTESIAN_POINT('Origin',(131.63578686942,-75.3686363338475,-196.851880310182)) ;
#81090=CARTESIAN_POINT('',(131.41353686942,-75.3686363338475,-197.090005310182)) ;
#81091=CARTESIAN_POINT('',(130.27053686942,-75.3686363338475,-197.090005310182)) ;
#81092=CARTESIAN_POINT('',(131.41353686942,-75.3686363338475,-197.090005310182)) ;
#81093=CARTESIAN_POINT('',(131.413536870957,-75.3686363338475,-198.36000531018)) ;
#81094=CARTESIAN_POINT('',(131.413536870572,-75.3686363338475,-198.36000531018)) ;
#81095=CARTESIAN_POINT('',(130.270536867883,-75.3686363338475,-198.36000531019)) ;
#81096=CARTESIAN_POINT('Origin',(130.84203686942,-75.3686363338475,-198.360005310182)) ;
#81097=CARTESIAN_POINT('',(130.27053686942,-75.3686363338475,-197.090005310182)) ;
#81098=CARTESIAN_POINT('Origin',(130.842036869357,-75.2733863367505,-198.360005310008)) ;
#81099=CARTESIAN_POINT('',(131.47703686942,-75.2733863338475,-198.360005310182)) ;
#81100=CARTESIAN_POINT('Origin',(131.572286870869,-75.2733863352967,-198.360005310175)) ;
#81101=CARTESIAN_POINT('',(130.20703686942,-75.2733863338475,-198.360005310177)) ;
#81102=CARTESIAN_POINT('Origin',(130.111786868103,-75.2733863351644,-198.360005310176)) ;
#81103=CARTESIAN_POINT('Origin',(130.84203686942,-75.2733863338475,-198.360005310182)) ;
#81104=CARTESIAN_POINT('Origin',(131.57228686942,-75.2733863338475,-198.360005310182)) ;
#81105=CARTESIAN_POINT('',(131.47703686942,-75.2733863338475,-197.090005310182)) ;
#81106=CARTESIAN_POINT('',(131.47703686942,-75.2733863338475,-198.360005310182)) ;
#81107=CARTESIAN_POINT('Origin',(131.57228686942,-75.2733863338475,-197.090005310182)) ;
#81108=CARTESIAN_POINT('Origin',(130.11178686942,-75.2733863338475,-196.994755310182)) ;
#81109=CARTESIAN_POINT('',(130.20703686942,-75.2733863338475,-197.090005310182)) ;
#81110=CARTESIAN_POINT('Origin',(130.11178686942,-75.2733863338475,-197.090005310182)) ;
#81111=CARTESIAN_POINT('',(130.20703686942,-75.2733863338475,-197.090005310182)) ;
#81112=CARTESIAN_POINT('Origin',(133.382036869594,-75.2733863367505,-200.90000531012)) ;
#81113=CARTESIAN_POINT('',(133.382036869419,-75.2733863338475,-201.535005310183)) ;
#81114=CARTESIAN_POINT('Origin',(133.382036869422,-75.2733863351644,-201.6302553115)) ;
#81115=CARTESIAN_POINT('',(133.382036869425,-75.2733863338475,-200.265005310183)) ;
#81116=CARTESIAN_POINT('Origin',(133.382036869425,-75.2733863351644,-200.169755308866)) ;
#81117=CARTESIAN_POINT('Origin',(133.38203686942,-75.2733863338475,-200.900005310183)) ;
#81118=CARTESIAN_POINT('Origin',(133.382036869419,-75.2733863338475,-201.630255310183)) ;
#81119=CARTESIAN_POINT('',(134.652036869419,-75.2733863338475,-201.535005310183)) ;
#81120=CARTESIAN_POINT('',(133.382036869419,-75.2733863338475,-201.535005310183)) ;
#81121=CARTESIAN_POINT('Origin',(134.652036869419,-75.2733863338475,-201.630255310183)) ;
#81122=CARTESIAN_POINT('Origin',(134.74728686942,-75.2733863338475,-200.169755310183)) ;
#81123=CARTESIAN_POINT('',(134.65203686942,-75.2733863338475,-200.265005310183)) ;
#81124=CARTESIAN_POINT('Origin',(134.65203686942,-75.2733863338475,-200.169755310183)) ;
#81125=CARTESIAN_POINT('',(134.65203686942,-75.2733863338475,-200.265005310183)) ;
#81126=CARTESIAN_POINT('Origin',(130.842036869482,-75.2733863367505,-203.440005310356)) ;
#81127=CARTESIAN_POINT('',(130.207036869419,-75.2733863338475,-203.440005310182)) ;
#81128=CARTESIAN_POINT('Origin',(130.11178686797,-75.2733863352967,-203.440005310189)) ;
#81129=CARTESIAN_POINT('',(131.477036869419,-75.2733863338475,-203.440005310188)) ;
#81130=CARTESIAN_POINT('Origin',(131.572286870736,-75.2733863351644,-203.440005310188)) ;
#81131=CARTESIAN_POINT('Origin',(130.842036869419,-75.2733863338475,-203.440005310182)) ;
#81132=CARTESIAN_POINT('Origin',(130.111786869419,-75.2733863338475,-203.440005310182)) ;
#81133=CARTESIAN_POINT('',(130.207036869419,-75.2733863338476,-204.710005310182)) ;
#81134=CARTESIAN_POINT('',(130.207036869419,-75.2733863338475,-203.440005310182)) ;
#81135=CARTESIAN_POINT('Origin',(130.111786869419,-75.2733863338475,-204.710005310182)) ;
#81136=CARTESIAN_POINT('Origin',(131.572286869419,-75.2733863338476,-204.805255310182)) ;
#81137=CARTESIAN_POINT('',(131.477036869419,-75.2733863338476,-204.710005310182)) ;
#81138=CARTESIAN_POINT('Origin',(131.572286869419,-75.2733863338476,-204.710005310182)) ;
#81139=CARTESIAN_POINT('',(131.477036869419,-75.2733863338476,-204.710005310182)) ;
#81140=CARTESIAN_POINT('Origin',(130.207036869419,-75.2733863338475,-203.440005310182)) ;
#81141=CARTESIAN_POINT('',(130.207036869419,-75.3051363338475,-203.440005310182)) ;
#81142=CARTESIAN_POINT('',(130.207036869419,-75.3051363338475,-204.710005310182)) ;
#81143=CARTESIAN_POINT('',(130.207036869419,-75.3051363338475,-203.440005310182)) ;
#81144=CARTESIAN_POINT('',(130.207036869419,-75.2733863338476,-204.710005310182)) ;
#81145=CARTESIAN_POINT('',(130.207036869419,-75.2733863338475,-203.440005310182)) ;
#81146=CARTESIAN_POINT('Origin',(131.477036869419,-75.2733863338476,-204.710005310182)) ;
#81147=CARTESIAN_POINT('',(131.477036869419,-75.3051363338475,-204.710005310182)) ;
#81148=CARTESIAN_POINT('',(131.477036869419,-75.3051363338475,-203.440005310185)) ;
#81149=CARTESIAN_POINT('',(131.477036869419,-75.3051363338475,-204.710005310182)) ;
#81150=CARTESIAN_POINT('',(131.477036869419,-75.2733863338475,-203.440005310188)) ;
#81151=CARTESIAN_POINT('',(131.477036869419,-75.2733863338476,-204.710005310182)) ;
#81152=CARTESIAN_POINT('Origin',(130.842036869419,-75.2733863338475,-203.440005310182)) ;
#81153=CARTESIAN_POINT('Origin',(130.842036869419,-75.3051363338475,-203.440005310182)) ;
#81154=CARTESIAN_POINT('Origin',(130.270536869419,-75.3051363338475,-203.440005310182)) ;
#81155=CARTESIAN_POINT('Origin',(130.270536868435,-75.3051363348312,-203.440005310183)) ;
#81156=CARTESIAN_POINT('Origin',(130.270536869419,-75.3051363338475,-204.710005310182)) ;
#81157=CARTESIAN_POINT('Origin',(131.413536869419,-75.3051363338475,-204.773505310182)) ;
#81158=CARTESIAN_POINT('Origin',(131.413536869419,-75.3051363338475,-204.710005310182)) ;
#81159=CARTESIAN_POINT('Origin',(131.413536870502,-75.3051363349301,-203.440005310169)) ;
#81160=CARTESIAN_POINT('Origin',(130.842036869372,-75.305136336016,-203.440005310312)) ;
#81161=CARTESIAN_POINT('Origin',(128.30203686942,-75.2733863338475,-200.265005310182)) ;
#81162=CARTESIAN_POINT('',(128.30203686942,-75.2733863338475,-200.265005310182)) ;
#81163=CARTESIAN_POINT('',(128.30203686942,-75.3051363338475,-200.265005310182)) ;
#81164=CARTESIAN_POINT('',(128.30203686942,-75.2733863338475,-200.265005310182)) ;
#81165=CARTESIAN_POINT('',(127.03203686942,-75.3051363338475,-200.265005310181)) ;
#81166=CARTESIAN_POINT('',(128.30203686942,-75.3051363338475,-200.265005310182)) ;
#81167=CARTESIAN_POINT('',(127.03203686942,-75.2733863338475,-200.265005310181)) ;
#81168=CARTESIAN_POINT('',(127.03203686942,-75.2733863338475,-200.265005310181)) ;
#81169=CARTESIAN_POINT('',(128.30203686942,-75.2733863338475,-200.265005310182)) ;
#81170=CARTESIAN_POINT('Origin',(127.032036869419,-75.2733863338475,-201.535005310181)) ;
#81171=CARTESIAN_POINT('',(127.032036869419,-75.2733863338475,-201.535005310181)) ;
#81172=CARTESIAN_POINT('',(127.032036869419,-75.3051363338475,-201.535005310181)) ;
#81173=CARTESIAN_POINT('',(127.032036869419,-75.2733863338475,-201.535005310181)) ;
#81174=CARTESIAN_POINT('',(128.302036869419,-75.3051363338475,-201.535005310182)) ;
#81175=CARTESIAN_POINT('',(127.032036869419,-75.3051363338475,-201.535005310181)) ;
#81176=CARTESIAN_POINT('',(128.302036869414,-75.2733863338475,-201.535005310182)) ;
#81177=CARTESIAN_POINT('',(128.302036869414,-75.2733863338475,-201.535005310182)) ;
#81178=CARTESIAN_POINT('',(127.032036869419,-75.2733863338475,-201.535005310181)) ;
#81179=CARTESIAN_POINT('Origin',(128.302036869289,-75.305136336016,-200.900005310135)) ;
#81180=CARTESIAN_POINT('Origin',(128.302036869425,-75.3051363348312,-201.471505311165)) ;
#81181=CARTESIAN_POINT('Origin',(128.302036869419,-75.3051363348312,-200.328505309198)) ;
#81182=CARTESIAN_POINT('Origin',(128.30203686942,-75.3051363338475,-200.900005310182)) ;
#81183=CARTESIAN_POINT('Origin',(128.30203686942,-75.3051363338475,-200.328505310182)) ;
#81184=CARTESIAN_POINT('Origin',(127.03203686942,-75.3051363338475,-200.328505310181)) ;
#81185=CARTESIAN_POINT('Origin',(126.968536869419,-75.3051363338475,-201.471505310181)) ;
#81186=CARTESIAN_POINT('Origin',(127.032036869419,-75.3051363338475,-201.471505310181)) ;
#81187=CARTESIAN_POINT('Origin',(131.47703686942,-75.2733863338475,-198.360005310182)) ;
#81188=CARTESIAN_POINT('',(131.47703686942,-75.3051363338475,-198.360005310182)) ;
#81189=CARTESIAN_POINT('',(131.47703686942,-75.3051363338475,-197.090005310182)) ;
#81190=CARTESIAN_POINT('',(131.47703686942,-75.3051363338475,-198.360005310182)) ;
#81191=CARTESIAN_POINT('',(131.47703686942,-75.2733863338475,-197.090005310182)) ;
#81192=CARTESIAN_POINT('',(131.47703686942,-75.2733863338475,-198.360005310182)) ;
#81193=CARTESIAN_POINT('Origin',(130.20703686942,-75.2733863338475,-197.090005310182)) ;
#81194=CARTESIAN_POINT('',(130.20703686942,-75.3051363338475,-197.090005310182)) ;
#81195=CARTESIAN_POINT('',(130.20703686942,-75.3051363338475,-198.360005310179)) ;
#81196=CARTESIAN_POINT('',(130.20703686942,-75.3051363338475,-197.090005310182)) ;
#81197=CARTESIAN_POINT('',(130.20703686942,-75.2733863338475,-198.360005310177)) ;
#81198=CARTESIAN_POINT('',(130.20703686942,-75.2733863338475,-197.090005310182)) ;
#81199=CARTESIAN_POINT('Origin',(130.84203686942,-75.2733863338475,-198.360005310182)) ;
#81200=CARTESIAN_POINT('Origin',(130.84203686942,-75.3051363338475,-198.360005310182)) ;
#81201=CARTESIAN_POINT('Origin',(130.842036869467,-75.305136336016,-198.360005310052)) ;
#81202=CARTESIAN_POINT('Origin',(130.270536868436,-75.3051363348312,-198.360005310185)) ;
#81203=CARTESIAN_POINT('Origin',(131.413536870404,-75.3051363348312,-198.360005310181)) ;
#81204=CARTESIAN_POINT('Origin',(131.41353686942,-75.3051363338475,-198.360005310182)) ;
#81205=CARTESIAN_POINT('Origin',(131.41353686942,-75.3051363338475,-197.090005310182)) ;
#81206=CARTESIAN_POINT('Origin',(130.27053686942,-75.3051363338475,-197.026505310182)) ;
#81207=CARTESIAN_POINT('Origin',(130.27053686942,-75.3051363338475,-197.090005310182)) ;
#81208=CARTESIAN_POINT('Origin',(133.382036869419,-75.2733863338475,-201.535005310183)) ;
#81209=CARTESIAN_POINT('',(133.382036869419,-75.3051363338475,-201.535005310183)) ;
#81210=CARTESIAN_POINT('',(134.652036869419,-75.3051363338475,-201.535005310183)) ;
#81211=CARTESIAN_POINT('',(133.382036869419,-75.3051363338475,-201.535005310183)) ;
#81212=CARTESIAN_POINT('',(134.652036869419,-75.2733863338475,-201.535005310183)) ;
#81213=CARTESIAN_POINT('',(133.382036869419,-75.2733863338475,-201.535005310183)) ;
#81214=CARTESIAN_POINT('Origin',(134.65203686942,-75.2733863338475,-200.265005310183)) ;
#81215=CARTESIAN_POINT('',(134.65203686942,-75.3051363338475,-200.265005310183)) ;
#81216=CARTESIAN_POINT('',(133.382036869422,-75.3051363338475,-200.265005310183)) ;
#81217=CARTESIAN_POINT('',(134.65203686942,-75.3051363338475,-200.265005310183)) ;
#81218=CARTESIAN_POINT('',(133.382036869425,-75.2733863338475,-200.265005310183)) ;
#81219=CARTESIAN_POINT('',(134.65203686942,-75.2733863338475,-200.265005310183)) ;
#81220=CARTESIAN_POINT('Origin',(133.38203686942,-75.2733863338475,-200.900005310183)) ;
#81221=CARTESIAN_POINT('Origin',(133.38203686942,-75.3051363338475,-200.900005310183)) ;
#81222=CARTESIAN_POINT('Origin',(133.382036869419,-75.3051363338475,-201.471505310183)) ;
#81223=CARTESIAN_POINT('Origin',(133.382036869421,-75.3051363348312,-201.471505311166)) ;
#81224=CARTESIAN_POINT('Origin',(134.652036869419,-75.3051363338475,-201.471505310183)) ;
#81225=CARTESIAN_POINT('Origin',(134.71553686942,-75.3051363338475,-200.328505310183)) ;
#81226=CARTESIAN_POINT('Origin',(134.65203686942,-75.3051363338475,-200.328505310183)) ;
#81227=CARTESIAN_POINT('Origin',(133.382036869407,-75.3051363349301,-200.3285053091)) ;
#81228=CARTESIAN_POINT('Origin',(133.38203686955,-75.305136336016,-200.90000531023)) ;
#81229=CARTESIAN_POINT('Origin',(128.30203686942,-75.2733863338475,-200.900005310182)) ;
#81230=CARTESIAN_POINT('Origin',(128.30203686942,-75.2733863338475,-200.900005310182)) ;
#81231=CARTESIAN_POINT('Origin',(128.302036869245,-75.2733863367505,-200.900005310245)) ;
#81232=CARTESIAN_POINT('Origin',(128.302036869417,-75.2733863351644,-200.169755308865)) ;
#81233=CARTESIAN_POINT('Origin',(128.302036869414,-75.2733863351644,-201.630255311499)) ;
#81234=CARTESIAN_POINT('Origin',(128.30203686942,-75.2733863338475,-200.169755310182)) ;
#81235=CARTESIAN_POINT('Origin',(127.03203686942,-75.2733863338475,-200.169755310181)) ;
#81236=CARTESIAN_POINT('Origin',(126.936786869419,-75.2733863338475,-201.630255310181)) ;
#81237=CARTESIAN_POINT('Origin',(127.032036869419,-75.2733863338475,-201.630255310181)) ;
#81238=CARTESIAN_POINT('Origin',(134.890161869419,-76.0036363338475,-201.693755310183)) ;
#81239=CARTESIAN_POINT('',(133.38203686942,-76.0036363338475,-200.454870310183)) ;
#81240=CARTESIAN_POINT('',(133.382036869419,-76.0036363338475,-201.345140310183)) ;
#81241=CARTESIAN_POINT('Origin',(133.38203686942,-76.0036363338475,-200.900005310183)) ;
#81242=CARTESIAN_POINT('',(134.652036869419,-76.0036363338475,-201.345140310183)) ;
#81243=CARTESIAN_POINT('',(133.382036869419,-76.0036363338475,-201.345140310183)) ;
#81244=CARTESIAN_POINT('',(134.65203686942,-76.0036363338475,-200.454870310183)) ;
#81245=CARTESIAN_POINT('',(134.652036869419,-76.0036363338475,-201.345140310183)) ;
#81246=CARTESIAN_POINT('',(134.65203686942,-76.0036363338475,-200.454870310183)) ;
#81247=CARTESIAN_POINT('Origin',(134.017036869419,-75.8131363338475,-201.535005310183)) ;
#81248=CARTESIAN_POINT('',(133.382036869419,-75.8134538337756,-201.535005257089)) ;
#81249=CARTESIAN_POINT('',(134.652036869419,-75.8131363338475,-201.535005310183)) ;
#81250=CARTESIAN_POINT('',(133.382036869419,-75.8131363338475,-201.535005310183)) ;
#81251=CARTESIAN_POINT('',(134.652036869419,-75.8137713338475,-201.535005310183)) ;
#81252=CARTESIAN_POINT('',(134.652036869419,-75.8131363338475,-201.535005310183)) ;
#81253=CARTESIAN_POINT('',(133.382036869419,-75.8137713338475,-201.535005310183)) ;
#81254=CARTESIAN_POINT('Origin',(134.01703686942,-75.8131363338475,-200.265005310183)) ;
#81255=CARTESIAN_POINT('',(134.65203686942,-75.8131363338475,-200.265005310183)) ;
#81256=CARTESIAN_POINT('',(134.65203686942,-75.8137713338475,-200.265005310183)) ;
#81257=CARTESIAN_POINT('',(134.65203686942,-75.8131363338475,-200.265005310183)) ;
#81258=CARTESIAN_POINT('',(133.38203686942,-75.8131363338475,-200.265005310183)) ;
#81259=CARTESIAN_POINT('',(134.65203686942,-75.8131363338475,-200.265005310183)) ;
#81260=CARTESIAN_POINT('',(133.38203686942,-75.8137713338475,-200.265005310183)) ;
#81261=CARTESIAN_POINT('',(133.38203686942,-75.8131363338475,-200.265005310183)) ;
#81262=CARTESIAN_POINT('',(134.65203686942,-75.8137713338475,-200.265005310183)) ;
#81263=CARTESIAN_POINT('Origin',(133.38203686942,-75.8131363338475,-200.900005310183)) ;
#81264=CARTESIAN_POINT('Origin',(133.38203686942,-75.8131363338475,-200.900005310183)) ;
#81265=CARTESIAN_POINT('Origin',(133.38203686942,-75.8137713338475,-200.900005310183)) ;
#81266=CARTESIAN_POINT('Origin',(134.111969369419,-75.8137713338475,-201.345140310183)) ;
#81267=CARTESIAN_POINT('Origin',(134.652036869419,-75.8137713338475,-201.345140310183)) ;
#81268=CARTESIAN_POINT('Origin',(133.382036869419,-75.8137713338475,-201.345140310183)) ;
#81269=CARTESIAN_POINT('Origin',(134.11196936942,-75.8137713338475,-200.454870310183)) ;
#81270=CARTESIAN_POINT('Origin',(133.38203686942,-75.8137713338475,-200.454870310183)) ;
#81271=CARTESIAN_POINT('Origin',(134.65203686942,-75.8137713338475,-200.454870310183)) ;
#81272=CARTESIAN_POINT('Origin',(133.38203686942,-75.8137713338475,-200.900005310183)) ;
#81273=CARTESIAN_POINT('Origin',(130.048286869419,-76.0036363338475,-204.948130310182)) ;
#81274=CARTESIAN_POINT('',(131.287171869419,-76.0036363338475,-203.440005310182)) ;
#81275=CARTESIAN_POINT('',(130.396901869419,-76.0036363338475,-203.440005310182)) ;
#81276=CARTESIAN_POINT('Origin',(130.842036869419,-76.0036363338475,-203.440005310182)) ;
#81277=CARTESIAN_POINT('',(130.396901869419,-76.0036363338475,-204.710005310182)) ;
#81278=CARTESIAN_POINT('',(130.396901869419,-76.0036363338475,-203.440005310182)) ;
#81279=CARTESIAN_POINT('',(131.287171869419,-76.0036363338475,-204.710005310182)) ;
#81280=CARTESIAN_POINT('',(130.396901869419,-76.0036363338475,-204.710005310182)) ;
#81281=CARTESIAN_POINT('',(131.287171869419,-76.0036363338475,-204.710005310182)) ;
#81282=CARTESIAN_POINT('Origin',(130.207036869419,-75.8131363338475,-204.075005310182)) ;
#81283=CARTESIAN_POINT('',(130.207036922513,-75.8134538337756,-203.440005310182)) ;
#81284=CARTESIAN_POINT('',(130.207036869419,-75.8131363338475,-204.710005310182)) ;
#81285=CARTESIAN_POINT('',(130.207036869419,-75.8131363338475,-203.440005310182)) ;
#81286=CARTESIAN_POINT('',(130.207036869419,-75.8137713338475,-204.710005310182)) ;
#81287=CARTESIAN_POINT('',(130.207036869419,-75.8131363338475,-204.710005310182)) ;
#81288=CARTESIAN_POINT('',(130.207036869419,-75.8137713338475,-203.440005310182)) ;
#81289=CARTESIAN_POINT('Origin',(131.477036869419,-75.8131363338475,-204.075005310182)) ;
#81290=CARTESIAN_POINT('',(131.477036869419,-75.8131363338475,-204.710005310182)) ;
#81291=CARTESIAN_POINT('',(131.477036869419,-75.8137713338475,-204.710005310182)) ;
#81292=CARTESIAN_POINT('',(131.477036869419,-75.8131363338475,-204.710005310182)) ;
#81293=CARTESIAN_POINT('',(131.477036869419,-75.8131363338475,-203.440005310182)) ;
#81294=CARTESIAN_POINT('',(131.477036869419,-75.8131363338475,-204.710005310182)) ;
#81295=CARTESIAN_POINT('',(131.477036869419,-75.8137713338475,-203.440005310182)) ;
#81296=CARTESIAN_POINT('',(131.477036869419,-75.8131363338475,-203.440005310182)) ;
#81297=CARTESIAN_POINT('',(131.477036869419,-75.8137713338475,-204.710005310182)) ;
#81298=CARTESIAN_POINT('Origin',(130.842036869419,-75.8131363338475,-203.440005310182)) ;
#81299=CARTESIAN_POINT('Origin',(130.842036869419,-75.8131363338475,-203.440005310182)) ;
#81300=CARTESIAN_POINT('Origin',(130.842036869419,-75.8137713338475,-203.440005310182)) ;
#81301=CARTESIAN_POINT('Origin',(130.396901869419,-75.8137713338475,-204.169937810182)) ;
#81302=CARTESIAN_POINT('Origin',(130.396901869419,-75.8137713338475,-204.710005310182)) ;
#81303=CARTESIAN_POINT('Origin',(130.396901869419,-75.8137713338475,-203.440005310182)) ;
#81304=CARTESIAN_POINT('Origin',(131.287171869419,-75.8137713338475,-204.169937810182)) ;
#81305=CARTESIAN_POINT('Origin',(131.287171869419,-75.8137713338475,-203.440005310182)) ;
#81306=CARTESIAN_POINT('Origin',(131.287171869419,-75.8137713338475,-204.710005310182)) ;
#81307=CARTESIAN_POINT('Origin',(130.842036869419,-75.8137713338475,-203.440005310182)) ;
#81308=CARTESIAN_POINT('Origin',(130.04828686942,-76.0036363338475,-196.851880310182)) ;
#81309=CARTESIAN_POINT('',(131.28717186942,-76.0036363338475,-197.090005310182)) ;
#81310=CARTESIAN_POINT('',(131.28717186942,-76.0036363338475,-198.360005310182)) ;
#81311=CARTESIAN_POINT('',(131.28717186942,-76.0036363338475,-197.090005310182)) ;
#81312=CARTESIAN_POINT('',(130.39690186942,-76.0036363338475,-197.090005310182)) ;
#81313=CARTESIAN_POINT('',(130.39690186942,-76.0036363338475,-197.090005310182)) ;
#81314=CARTESIAN_POINT('',(130.39690186942,-76.0036363338475,-198.360005310182)) ;
#81315=CARTESIAN_POINT('',(130.39690186942,-76.0036363338475,-198.360005310182)) ;
#81316=CARTESIAN_POINT('Origin',(130.84203686942,-76.0036363338475,-198.360005310182)) ;
#81317=CARTESIAN_POINT('Origin',(130.20703686942,-75.9083863338475,-198.360005310182)) ;
#81318=CARTESIAN_POINT('',(130.207036922514,-75.8134538337756,-198.360005310182)) ;
#81319=CARTESIAN_POINT('',(130.20703686942,-75.8137713338475,-197.090005310182)) ;
#81320=CARTESIAN_POINT('',(130.20703686942,-75.8137713338475,-198.360005310182)) ;
#81321=CARTESIAN_POINT('',(130.20703686942,-75.8131363338475,-197.090005310182)) ;
#81322=CARTESIAN_POINT('',(130.20703686942,-75.8131363338475,-197.090005310182)) ;
#81323=CARTESIAN_POINT('',(130.20703686942,-75.8131363338475,-197.090005310182)) ;
#81324=CARTESIAN_POINT('Origin',(131.47703686942,-75.9083863338475,-197.090005310182)) ;
#81325=CARTESIAN_POINT('',(131.47703686942,-75.8137713338475,-197.090005310182)) ;
#81326=CARTESIAN_POINT('',(131.47703686942,-75.8137713338475,-198.360005310182)) ;
#81327=CARTESIAN_POINT('',(131.47703686942,-75.8137713338475,-197.090005310182)) ;
#81328=CARTESIAN_POINT('',(131.47703686942,-75.8131363338475,-198.360005310182)) ;
#81329=CARTESIAN_POINT('',(131.47703686942,-75.8131363338475,-198.360005310182)) ;
#81330=CARTESIAN_POINT('',(131.47703686942,-75.8131363338475,-197.090005310182)) ;
#81331=CARTESIAN_POINT('',(131.47703686942,-75.8131363338475,-198.360005310182)) ;
#81332=CARTESIAN_POINT('',(131.47703686942,-75.8131363338475,-197.090005310182)) ;
#81333=CARTESIAN_POINT('Origin',(130.84203686942,-75.9083863338475,-198.360005310182)) ;
#81334=CARTESIAN_POINT('Origin',(130.84203686942,-75.8137713338475,-198.360005310182)) ;
#81335=CARTESIAN_POINT('Origin',(130.84203686942,-75.8131363338475,-198.360005310182)) ;
#81336=CARTESIAN_POINT('Origin',(130.39690186942,-75.8137713338475,-198.360005310182)) ;
#81337=CARTESIAN_POINT('Origin',(130.39690186942,-75.8137713338475,-198.360005310182)) ;
#81338=CARTESIAN_POINT('Origin',(130.39690186942,-75.8137713338475,-197.090005310182)) ;
#81339=CARTESIAN_POINT('Origin',(131.28717186942,-75.8137713338475,-196.900140310182)) ;
#81340=CARTESIAN_POINT('Origin',(131.28717186942,-75.8137713338475,-197.090005310182)) ;
#81341=CARTESIAN_POINT('Origin',(131.28717186942,-75.8137713338475,-198.360005310182)) ;
#81342=CARTESIAN_POINT('Origin',(130.84203686942,-75.8137713338475,-198.360005310182)) ;
#81343=CARTESIAN_POINT('Origin',(126.793911869419,-76.0036363338475,-201.693755310181)) ;
#81344=CARTESIAN_POINT('',(127.03203686942,-76.0036363338475,-200.454870310181)) ;
#81345=CARTESIAN_POINT('',(128.30203686942,-76.0036363338475,-200.454870310182)) ;
#81346=CARTESIAN_POINT('',(127.03203686942,-76.0036363338475,-200.454870310181)) ;
#81347=CARTESIAN_POINT('',(127.032036869419,-76.0036363338475,-201.345140310181)) ;
#81348=CARTESIAN_POINT('',(127.032036869419,-76.0036363338475,-201.345140310181)) ;
#81349=CARTESIAN_POINT('',(128.302036869419,-76.0036363338475,-201.345140310182)) ;
#81350=CARTESIAN_POINT('',(128.302036869419,-76.0036363338475,-201.345140310182)) ;
#81351=CARTESIAN_POINT('Origin',(128.30203686942,-76.0036363338475,-200.900005310182)) ;
#81352=CARTESIAN_POINT('Origin',(128.302036869419,-75.9083863338475,-201.535005310182)) ;
#81353=CARTESIAN_POINT('',(128.302036869419,-75.8134538337756,-201.535005257088)) ;
#81354=CARTESIAN_POINT('',(127.032036869419,-75.8137713338475,-201.535005310181)) ;
#81355=CARTESIAN_POINT('',(128.302036869419,-75.8137713338475,-201.535005310182)) ;
#81356=CARTESIAN_POINT('',(127.032036869419,-75.8131363338475,-201.535005310181)) ;
#81357=CARTESIAN_POINT('',(127.032036869419,-75.8131363338475,-201.535005310181)) ;
#81358=CARTESIAN_POINT('',(127.032036869419,-75.8131363338475,-201.535005310181)) ;
#81359=CARTESIAN_POINT('Origin',(127.03203686942,-75.9083863338475,-200.265005310181)) ;
#81360=CARTESIAN_POINT('',(127.03203686942,-75.8137713338475,-200.265005310181)) ;
#81361=CARTESIAN_POINT('',(128.30203686942,-75.8137713338475,-200.265005310182)) ;
#81362=CARTESIAN_POINT('',(127.03203686942,-75.8137713338475,-200.265005310181)) ;
#81363=CARTESIAN_POINT('',(128.30203686942,-75.8131363338475,-200.265005310182)) ;
#81364=CARTESIAN_POINT('',(128.30203686942,-75.8131363338475,-200.265005310182)) ;
#81365=CARTESIAN_POINT('',(127.03203686942,-75.8131363338475,-200.265005310181)) ;
#81366=CARTESIAN_POINT('',(128.30203686942,-75.8131363338475,-200.265005310182)) ;
#81367=CARTESIAN_POINT('',(127.03203686942,-75.8131363338475,-200.265005310181)) ;
#81368=CARTESIAN_POINT('Origin',(128.30203686942,-75.9083863338475,-200.900005310182)) ;
#81369=CARTESIAN_POINT('Origin',(128.30203686942,-75.8137713338475,-200.900005310182)) ;
#81370=CARTESIAN_POINT('Origin',(128.30203686942,-75.8131363338475,-200.900005310182)) ;
#81371=CARTESIAN_POINT('Origin',(128.302036869419,-75.8137713338475,-201.345140310182)) ;
#81372=CARTESIAN_POINT('Origin',(128.302036869419,-75.8137713338475,-201.345140310182)) ;
#81373=CARTESIAN_POINT('Origin',(127.032036869419,-75.8137713338475,-201.345140310181)) ;
#81374=CARTESIAN_POINT('Origin',(126.84217186942,-75.8137713338475,-200.454870310181)) ;
#81375=CARTESIAN_POINT('Origin',(127.03203686942,-75.8137713338475,-200.454870310181)) ;
#81376=CARTESIAN_POINT('Origin',(128.30203686942,-75.8137713338475,-200.454870310182)) ;
#81377=CARTESIAN_POINT('Origin',(128.30203686942,-75.8137713338475,-200.900005310182)) ;
#81378=CARTESIAN_POINT('Origin',(134.652036869419,-75.1781363338475,-204.710005310183)) ;
#81379=CARTESIAN_POINT('',(134.652036869419,-75.8131363338476,-204.481982804729)) ;
#81380=CARTESIAN_POINT('',(134.652036869419,-75.8131363338476,-204.481982804729)) ;
#81381=CARTESIAN_POINT('',(134.65203686942,-75.8131363338475,-197.318027815637)) ;
#81382=CARTESIAN_POINT('',(134.65203686942,-75.2257613338475,-197.318027815637)) ;
#81383=CARTESIAN_POINT('',(134.65203686942,-75.8131363338475,-198.058109844874)) ;
#81384=CARTESIAN_POINT('',(134.65203686942,-75.8131363338475,-198.058109844874)) ;
#81385=CARTESIAN_POINT('',(134.65203686942,-75.8131363338475,-200.265005310183)) ;
#81386=CARTESIAN_POINT('',(134.652036869419,-75.8131363338475,-203.741900775492)) ;
#81387=CARTESIAN_POINT('',(134.652036869419,-75.8131363338475,-203.741900775492)) ;
#81388=CARTESIAN_POINT('',(134.652036869419,-75.8131363338476,-204.481982804729)) ;
#81389=CARTESIAN_POINT('Origin',(127.03203686942,-75.1781363338475,-197.090005310181)) ;
#81390=CARTESIAN_POINT('',(127.03203686942,-75.8131363338475,-197.318027815635)) ;
#81391=CARTESIAN_POINT('',(127.03203686942,-75.8131363338475,-197.318027815635)) ;
#81392=CARTESIAN_POINT('',(127.032036869419,-75.8131363338475,-204.481982804728)) ;
#81393=CARTESIAN_POINT('',(127.032036869419,-75.2257613338475,-204.481982804728)) ;
#81394=CARTESIAN_POINT('',(127.032036869419,-75.8131363338475,-203.741900775491)) ;
#81395=CARTESIAN_POINT('',(127.032036869419,-75.8131363338475,-203.741900775491)) ;
#81396=CARTESIAN_POINT('',(127.032036869419,-75.8131363338475,-201.535005310181)) ;
#81397=CARTESIAN_POINT('',(127.03203686942,-75.8131363338475,-198.058109844872)) ;
#81398=CARTESIAN_POINT('',(127.03203686942,-75.8131363338475,-198.058109844872)) ;
#81399=CARTESIAN_POINT('',(127.03203686942,-75.8131363338475,-197.318027815635)) ;
#81400=CARTESIAN_POINT('Origin',(127.032036869419,-75.1781363338475,-204.710005310181)) ;
#81401=CARTESIAN_POINT('',(127.260059374872,-75.8131363338475,-204.710005310181)) ;
#81402=CARTESIAN_POINT('',(127.260059374872,-75.8131363338475,-204.710005310181)) ;
#81403=CARTESIAN_POINT('',(134.424014363965,-75.8131363338476,-204.710005310183)) ;
#81404=CARTESIAN_POINT('',(134.424014363965,-75.2257613338475,-204.710005310183)) ;
#81405=CARTESIAN_POINT('',(133.683932334728,-75.8131363338475,-204.710005310183)) ;
#81406=CARTESIAN_POINT('',(133.683932334728,-75.8131363338475,-204.710005310183)) ;
#81407=CARTESIAN_POINT('',(131.477036869419,-75.8131363338475,-204.710005310182)) ;
#81408=CARTESIAN_POINT('',(128.000141404109,-75.8131363338475,-204.710005310182)) ;
#81409=CARTESIAN_POINT('',(128.000141404109,-75.8131363338475,-204.710005310182)) ;
#81410=CARTESIAN_POINT('',(127.260059374872,-75.8131363338475,-204.710005310181)) ;
#81411=CARTESIAN_POINT('Origin',(134.65203686942,-75.1781363338475,-197.090005310183)) ;
#81412=CARTESIAN_POINT('',(134.424014363967,-75.8131363338475,-197.090005310183)) ;
#81413=CARTESIAN_POINT('',(134.424014363967,-75.8131363338475,-197.090005310183)) ;
#81414=CARTESIAN_POINT('',(127.260059374874,-75.8131363338475,-197.090005310181)) ;
#81415=CARTESIAN_POINT('',(127.260059356689,-75.2257613340712,-197.090005310181)) ;
#81416=CARTESIAN_POINT('',(128.000141404111,-75.8131363338475,-197.090005310182)) ;
#81417=CARTESIAN_POINT('',(128.000141404111,-75.8131363338475,-197.090005310182)) ;
#81418=CARTESIAN_POINT('',(130.20703686942,-75.8131363338475,-197.090005310182)) ;
#81419=CARTESIAN_POINT('',(133.683932334729,-75.8131363338475,-197.090005310183)) ;
#81420=CARTESIAN_POINT('',(133.683932334729,-75.8131363338475,-197.090005310183)) ;
#81421=CARTESIAN_POINT('',(134.424014363967,-75.8131363338475,-197.090005310183)) ;
#81422=CARTESIAN_POINT('Origin',(134.65203686942,-75.8131363338475,-197.090005310183)) ;
#81423=CARTESIAN_POINT('Origin',(130.84203686942,-75.8131363338476,-200.900005310182)) ;
#81424=CARTESIAN_POINT('',(127.481049604646,-75.8131363338475,-197.539018187062)) ;
#81425=CARTESIAN_POINT('Origin',(130.84203686942,-75.8131363338478,-200.900005310182)) ;
#81426=CARTESIAN_POINT('Origin',(130.84203686942,-75.8131363338475,-200.900005310182)) ;
#81427=CARTESIAN_POINT('Origin',(130.84203686942,-75.8131363338475,-200.900005310182)) ;
#81428=CARTESIAN_POINT('Origin',(130.84203686942,-75.8131363338476,-200.900005310182)) ;
#81429=CARTESIAN_POINT('Ctrl Pts',(127.032036789131,-76.0036363338475,-197.090005390471)) ;
#81430=CARTESIAN_POINT('Ctrl Pts',(127.032036789131,-75.8131363338475,-197.090005390471)) ;
#81431=CARTESIAN_POINT('Ctrl Pts',(127.481049604646,-75.8131363338475,-197.539018187062)) ;
#81432=CARTESIAN_POINT('Ctrl Pts',(123.222036869419,-76.0036363338475,-200.90000547076)) ;
#81433=CARTESIAN_POINT('Ctrl Pts',(123.222036869419,-75.8131363338475,-200.90000547076)) ;
#81434=CARTESIAN_POINT('Ctrl Pts',(124.120062481526,-75.8131363338475,-200.900005451836)) ;
#81435=CARTESIAN_POINT('Ctrl Pts',(127.032036949709,-76.0036363338475,-204.710005390471)) ;
#81436=CARTESIAN_POINT('Ctrl Pts',(127.032036949709,-75.8131363338475,-204.710005390471)) ;
#81437=CARTESIAN_POINT('Ctrl Pts',(127.4810497463,-75.8131363338475,-204.260992574956)) ;
#81438=CARTESIAN_POINT('Ctrl Pts',(130.842037029998,-76.0036363338476,-208.520005310182)) ;
#81439=CARTESIAN_POINT('Ctrl Pts',(130.842037029998,-75.8131363338476,-208.520005310182)) ;
#81440=CARTESIAN_POINT('Ctrl Pts',(130.842037011073,-75.8131363338476,-207.621979698075)) ;
#81441=CARTESIAN_POINT('Ctrl Pts',(134.652036949709,-76.0036363338476,-204.710005229893)) ;
#81442=CARTESIAN_POINT('Ctrl Pts',(134.652036949709,-75.8131363338476,-204.710005229893)) ;
#81443=CARTESIAN_POINT('Ctrl Pts',(134.203024134193,-75.8131363338476,-204.260992433302)) ;
#81444=CARTESIAN_POINT('Ctrl Pts',(138.46203686942,-76.0036363338475,-200.900005149604)) ;
#81445=CARTESIAN_POINT('Ctrl Pts',(138.46203686942,-75.8131363338475,-200.900005149604)) ;
#81446=CARTESIAN_POINT('Ctrl Pts',(137.564011257313,-75.8131363338475,-200.900005168529)) ;
#81447=CARTESIAN_POINT('Ctrl Pts',(134.652036789131,-76.0036363338475,-197.090005229893)) ;
#81448=CARTESIAN_POINT('Ctrl Pts',(134.652036789131,-75.8131363338475,-197.090005229893)) ;
#81449=CARTESIAN_POINT('Ctrl Pts',(134.203023992539,-75.8131363338475,-197.539018045409)) ;
#81450=CARTESIAN_POINT('Ctrl Pts',(130.842036708842,-76.0036363338475,-193.280005310182)) ;
#81451=CARTESIAN_POINT('Ctrl Pts',(130.842036708842,-75.8131363338475,-193.280005310182)) ;
#81452=CARTESIAN_POINT('Ctrl Pts',(130.842036727766,-75.8131363338475,-194.178030922289)) ;
#81453=CARTESIAN_POINT('Ctrl Pts',(127.032036789131,-76.0036363338475,-197.090005390471)) ;
#81454=CARTESIAN_POINT('Ctrl Pts',(127.032036789131,-75.8131363338475,-197.090005390471)) ;
#81455=CARTESIAN_POINT('Ctrl Pts',(127.481049604646,-75.8131363338475,-197.539018187062)) ;
#81456=CARTESIAN_POINT('',(134.424014372653,-75.8607613348135,-204.710005308452)) ;
#81457=CARTESIAN_POINT('',(134.652036871149,-75.8607613328816,-204.481982796042)) ;
#81458=CARTESIAN_POINT('Origin',(130.842036868431,-75.8607613338483,-200.90000531117)) ;
#81459=CARTESIAN_POINT('Ctrl Pts',(134.652036869419,-75.8607613320955,-204.481982796203)) ;
#81460=CARTESIAN_POINT('Ctrl Pts',(134.652036869419,-75.8396272026366,-204.379135603943)) ;
#81461=CARTESIAN_POINT('Ctrl Pts',(134.652036869522,-75.8281624630209,-204.252864864675)) ;
#81462=CARTESIAN_POINT('Ctrl Pts',(134.652036869522,-75.8151140186796,-204.001616634739)) ;
#81463=CARTESIAN_POINT('Ctrl Pts',(134.652036869419,-75.8131363338476,-203.866854124742)) ;
#81464=CARTESIAN_POINT('Ctrl Pts',(134.652036869419,-75.8131363338476,-203.741900775492)) ;
#81465=CARTESIAN_POINT('Ctrl Pts',(133.683932334728,-75.8131363338476,-204.710005310182)) ;
#81466=CARTESIAN_POINT('Ctrl Pts',(133.808883891339,-75.8131363338476,-204.710005310182)) ;
#81467=CARTESIAN_POINT('Ctrl Pts',(133.943644060714,-75.8151139619344,-204.710005310299)) ;
#81468=CARTESIAN_POINT('Ctrl Pts',(134.194888618251,-75.8281618997334,-204.710005310299)) ;
#81469=CARTESIAN_POINT('Ctrl Pts',(134.32116760723,-75.8396272922766,-204.710005310183)) ;
#81470=CARTESIAN_POINT('Ctrl Pts',(134.424014372491,-75.8607613355995,-204.710005310183)) ;
#81471=CARTESIAN_POINT('Origin',(134.652036869419,-75.8131363338476,-204.710005310183)) ;
#81472=CARTESIAN_POINT('',(134.652036869419,-75.860761333691,-204.481982792)) ;
#81473=CARTESIAN_POINT('Origin',(127.032036869419,-75.8131363338475,-204.710005310181)) ;
#81474=CARTESIAN_POINT('',(134.424014363965,-75.8131363338476,-204.710005310183)) ;
#81475=CARTESIAN_POINT('Ctrl Pts',(127.032036789131,-76.0036363338475,-197.090005390471)) ;
#81476=CARTESIAN_POINT('Ctrl Pts',(127.032036789131,-75.8131363338475,-197.090005390471)) ;
#81477=CARTESIAN_POINT('Ctrl Pts',(127.481049604646,-75.8131363338475,-197.539018187062)) ;
#81478=CARTESIAN_POINT('Ctrl Pts',(123.222036869419,-76.0036363338475,-200.90000547076)) ;
#81479=CARTESIAN_POINT('Ctrl Pts',(123.222036869419,-75.8131363338475,-200.90000547076)) ;
#81480=CARTESIAN_POINT('Ctrl Pts',(124.120062481526,-75.8131363338475,-200.900005451836)) ;
#81481=CARTESIAN_POINT('Ctrl Pts',(127.032036949709,-76.0036363338475,-204.710005390471)) ;
#81482=CARTESIAN_POINT('Ctrl Pts',(127.032036949709,-75.8131363338475,-204.710005390471)) ;
#81483=CARTESIAN_POINT('Ctrl Pts',(127.4810497463,-75.8131363338475,-204.260992574956)) ;
#81484=CARTESIAN_POINT('Ctrl Pts',(130.842037029998,-76.0036363338476,-208.520005310182)) ;
#81485=CARTESIAN_POINT('Ctrl Pts',(130.842037029998,-75.8131363338476,-208.520005310182)) ;
#81486=CARTESIAN_POINT('Ctrl Pts',(130.842037011073,-75.8131363338476,-207.621979698075)) ;
#81487=CARTESIAN_POINT('Ctrl Pts',(134.652036949709,-76.0036363338476,-204.710005229893)) ;
#81488=CARTESIAN_POINT('Ctrl Pts',(134.652036949709,-75.8131363338476,-204.710005229893)) ;
#81489=CARTESIAN_POINT('Ctrl Pts',(134.203024134193,-75.8131363338476,-204.260992433302)) ;
#81490=CARTESIAN_POINT('Ctrl Pts',(138.46203686942,-76.0036363338475,-200.900005149604)) ;
#81491=CARTESIAN_POINT('Ctrl Pts',(138.46203686942,-75.8131363338475,-200.900005149604)) ;
#81492=CARTESIAN_POINT('Ctrl Pts',(137.564011257313,-75.8131363338475,-200.900005168529)) ;
#81493=CARTESIAN_POINT('Ctrl Pts',(134.652036789131,-76.0036363338475,-197.090005229893)) ;
#81494=CARTESIAN_POINT('Ctrl Pts',(134.652036789131,-75.8131363338475,-197.090005229893)) ;
#81495=CARTESIAN_POINT('Ctrl Pts',(134.203023992539,-75.8131363338475,-197.539018045409)) ;
#81496=CARTESIAN_POINT('Ctrl Pts',(130.842036708842,-76.0036363338475,-193.280005310182)) ;
#81497=CARTESIAN_POINT('Ctrl Pts',(130.842036708842,-75.8131363338475,-193.280005310182)) ;
#81498=CARTESIAN_POINT('Ctrl Pts',(130.842036727766,-75.8131363338475,-194.178030922289)) ;
#81499=CARTESIAN_POINT('Ctrl Pts',(127.032036789131,-76.0036363338475,-197.090005390471)) ;
#81500=CARTESIAN_POINT('Ctrl Pts',(127.032036789131,-75.8131363338475,-197.090005390471)) ;
#81501=CARTESIAN_POINT('Ctrl Pts',(127.481049604646,-75.8131363338475,-197.539018187062)) ;
#81502=CARTESIAN_POINT('',(127.032036871149,-75.8607613348136,-204.481982813415)) ;
#81503=CARTESIAN_POINT('',(127.26005938356,-75.8607613328816,-204.710005311911)) ;
#81504=CARTESIAN_POINT('Origin',(130.842036868431,-75.8607613338468,-200.900005309194)) ;
#81505=CARTESIAN_POINT('Ctrl Pts',(127.260059383398,-75.8607613320955,-204.710005310181)) ;
#81506=CARTESIAN_POINT('Ctrl Pts',(127.362906575657,-75.8396272026369,-204.710005310181)) ;
#81507=CARTESIAN_POINT('Ctrl Pts',(127.489177314922,-75.8281624630211,-204.710005310284)) ;
#81508=CARTESIAN_POINT('Ctrl Pts',(127.74042554486,-75.8151140186795,-204.710005310284)) ;
#81509=CARTESIAN_POINT('Ctrl Pts',(127.875188054858,-75.8131363338475,-204.710005310181)) ;
#81510=CARTESIAN_POINT('Ctrl Pts',(128.000141404109,-75.8131363338475,-204.710005310181)) ;
#81511=CARTESIAN_POINT('Ctrl Pts',(127.032036869419,-75.8131363338475,-203.741900775491)) ;
#81512=CARTESIAN_POINT('Ctrl Pts',(127.032036869419,-75.8131363338475,-203.866852332103)) ;
#81513=CARTESIAN_POINT('Ctrl Pts',(127.032036869302,-75.8151139619343,-204.001612501477)) ;
#81514=CARTESIAN_POINT('Ctrl Pts',(127.032036869302,-75.8281618997335,-204.252857059014)) ;
#81515=CARTESIAN_POINT('Ctrl Pts',(127.032036869419,-75.8396272922767,-204.379136047993)) ;
#81516=CARTESIAN_POINT('Ctrl Pts',(127.032036869419,-75.8607613355997,-204.481982813254)) ;
#81517=CARTESIAN_POINT('Origin',(127.03203686942,-75.8131363338475,-197.090005310181)) ;
#81518=CARTESIAN_POINT('',(127.032036869419,-75.8131363338475,-204.481982804728)) ;
#81519=CARTESIAN_POINT('Origin',(127.032036869419,-75.8131363338475,-204.710005310181)) ;
#81520=CARTESIAN_POINT('',(127.260059387602,-75.860761333691,-204.710005310181)) ;
#81521=CARTESIAN_POINT('Ctrl Pts',(127.032036789131,-76.0036363338475,-197.090005390471)) ;
#81522=CARTESIAN_POINT('Ctrl Pts',(127.032036789131,-75.8131363338475,-197.090005390471)) ;
#81523=CARTESIAN_POINT('Ctrl Pts',(127.481049604646,-75.8131363338475,-197.539018187062)) ;
#81524=CARTESIAN_POINT('Ctrl Pts',(123.222036869419,-76.0036363338475,-200.90000547076)) ;
#81525=CARTESIAN_POINT('Ctrl Pts',(123.222036869419,-75.8131363338475,-200.90000547076)) ;
#81526=CARTESIAN_POINT('Ctrl Pts',(124.120062481526,-75.8131363338475,-200.900005451836)) ;
#81527=CARTESIAN_POINT('Ctrl Pts',(127.032036949709,-76.0036363338475,-204.710005390471)) ;
#81528=CARTESIAN_POINT('Ctrl Pts',(127.032036949709,-75.8131363338475,-204.710005390471)) ;
#81529=CARTESIAN_POINT('Ctrl Pts',(127.4810497463,-75.8131363338475,-204.260992574956)) ;
#81530=CARTESIAN_POINT('Ctrl Pts',(130.842037029998,-76.0036363338476,-208.520005310182)) ;
#81531=CARTESIAN_POINT('Ctrl Pts',(130.842037029998,-75.8131363338476,-208.520005310182)) ;
#81532=CARTESIAN_POINT('Ctrl Pts',(130.842037011073,-75.8131363338476,-207.621979698075)) ;
#81533=CARTESIAN_POINT('Ctrl Pts',(134.652036949709,-76.0036363338476,-204.710005229893)) ;
#81534=CARTESIAN_POINT('Ctrl Pts',(134.652036949709,-75.8131363338476,-204.710005229893)) ;
#81535=CARTESIAN_POINT('Ctrl Pts',(134.203024134193,-75.8131363338476,-204.260992433302)) ;
#81536=CARTESIAN_POINT('Ctrl Pts',(138.46203686942,-76.0036363338475,-200.900005149604)) ;
#81537=CARTESIAN_POINT('Ctrl Pts',(138.46203686942,-75.8131363338475,-200.900005149604)) ;
#81538=CARTESIAN_POINT('Ctrl Pts',(137.564011257313,-75.8131363338475,-200.900005168529)) ;
#81539=CARTESIAN_POINT('Ctrl Pts',(134.652036789131,-76.0036363338475,-197.090005229893)) ;
#81540=CARTESIAN_POINT('Ctrl Pts',(134.652036789131,-75.8131363338475,-197.090005229893)) ;
#81541=CARTESIAN_POINT('Ctrl Pts',(134.203023992539,-75.8131363338475,-197.539018045409)) ;
#81542=CARTESIAN_POINT('Ctrl Pts',(130.842036708842,-76.0036363338475,-193.280005310182)) ;
#81543=CARTESIAN_POINT('Ctrl Pts',(130.842036708842,-75.8131363338475,-193.280005310182)) ;
#81544=CARTESIAN_POINT('Ctrl Pts',(130.842036727766,-75.8131363338475,-194.178030922289)) ;
#81545=CARTESIAN_POINT('Ctrl Pts',(127.032036789131,-76.0036363338475,-197.090005390471)) ;
#81546=CARTESIAN_POINT('Ctrl Pts',(127.032036789131,-75.8131363338475,-197.090005390471)) ;
#81547=CARTESIAN_POINT('Ctrl Pts',(127.481049604646,-75.8131363338475,-197.539018187062)) ;
#81548=CARTESIAN_POINT('',(127.144290007455,-75.8607613338475,-197.202258575173)) ;
#81549=CARTESIAN_POINT('',(127.032036867121,-75.8607613325238,-197.318027827715)) ;
#81550=CARTESIAN_POINT('Origin',(130.842036777866,-75.86076129501,-200.900005218629)) ;
#81551=CARTESIAN_POINT('Ctrl Pts',(127.03203686942,-75.8607613314121,-197.318027827487)) ;
#81552=CARTESIAN_POINT('Ctrl Pts',(127.03203686942,-75.8396272023282,-197.420875019448)) ;
#81553=CARTESIAN_POINT('Ctrl Pts',(127.032036869317,-75.8281624628045,-197.547145758675)) ;
#81554=CARTESIAN_POINT('Ctrl Pts',(127.032036869317,-75.8151140186575,-197.798393987228)) ;
#81555=CARTESIAN_POINT('Ctrl Pts',(127.03203686942,-75.8131363338475,-197.933156496317)) ;
#81556=CARTESIAN_POINT('Ctrl Pts',(127.03203686942,-75.8131363338475,-198.058109844872)) ;
#81557=CARTESIAN_POINT('Ctrl Pts',(127.144290007455,-75.8607613338475,-197.202258575173)) ;
#81558=CARTESIAN_POINT('Ctrl Pts',(127.2191254716,-75.8290113338475,-197.277094046379)) ;
#81559=CARTESIAN_POINT('Ctrl Pts',(127.331378670518,-75.8131363338475,-197.389347250489)) ;
#81560=CARTESIAN_POINT('Ctrl Pts',(127.481049604646,-75.8131363338475,-197.539018187062)) ;
#81561=CARTESIAN_POINT('Ctrl Pts',(127.032036789131,-76.0036363338475,-197.090005390471)) ;
#81562=CARTESIAN_POINT('Ctrl Pts',(127.032036789131,-75.8131363338475,-197.090005390471)) ;
#81563=CARTESIAN_POINT('Ctrl Pts',(127.481049604646,-75.8131363338475,-197.539018187062)) ;
#81564=CARTESIAN_POINT('Ctrl Pts',(123.222036869419,-76.0036363338475,-200.90000547076)) ;
#81565=CARTESIAN_POINT('Ctrl Pts',(123.222036869419,-75.8131363338475,-200.90000547076)) ;
#81566=CARTESIAN_POINT('Ctrl Pts',(124.120062481526,-75.8131363338475,-200.900005451836)) ;
#81567=CARTESIAN_POINT('Ctrl Pts',(127.032036949709,-76.0036363338475,-204.710005390471)) ;
#81568=CARTESIAN_POINT('Ctrl Pts',(127.032036949709,-75.8131363338475,-204.710005390471)) ;
#81569=CARTESIAN_POINT('Ctrl Pts',(127.4810497463,-75.8131363338475,-204.260992574956)) ;
#81570=CARTESIAN_POINT('Ctrl Pts',(130.842037029998,-76.0036363338476,-208.520005310182)) ;
#81571=CARTESIAN_POINT('Ctrl Pts',(130.842037029998,-75.8131363338476,-208.520005310182)) ;
#81572=CARTESIAN_POINT('Ctrl Pts',(130.842037011073,-75.8131363338476,-207.621979698075)) ;
#81573=CARTESIAN_POINT('Ctrl Pts',(134.652036949709,-76.0036363338476,-204.710005229893)) ;
#81574=CARTESIAN_POINT('Ctrl Pts',(134.652036949709,-75.8131363338476,-204.710005229893)) ;
#81575=CARTESIAN_POINT('Ctrl Pts',(134.203024134193,-75.8131363338476,-204.260992433302)) ;
#81576=CARTESIAN_POINT('Ctrl Pts',(138.46203686942,-76.0036363338475,-200.900005149604)) ;
#81577=CARTESIAN_POINT('Ctrl Pts',(138.46203686942,-75.8131363338475,-200.900005149604)) ;
#81578=CARTESIAN_POINT('Ctrl Pts',(137.564011257313,-75.8131363338475,-200.900005168529)) ;
#81579=CARTESIAN_POINT('Ctrl Pts',(134.652036789131,-76.0036363338475,-197.090005229893)) ;
#81580=CARTESIAN_POINT('Ctrl Pts',(134.652036789131,-75.8131363338475,-197.090005229893)) ;
#81581=CARTESIAN_POINT('Ctrl Pts',(134.203023992539,-75.8131363338475,-197.539018045409)) ;
#81582=CARTESIAN_POINT('Ctrl Pts',(130.842036708842,-76.0036363338475,-193.280005310182)) ;
#81583=CARTESIAN_POINT('Ctrl Pts',(130.842036708842,-75.8131363338475,-193.280005310182)) ;
#81584=CARTESIAN_POINT('Ctrl Pts',(130.842036727766,-75.8131363338475,-194.178030922289)) ;
#81585=CARTESIAN_POINT('Ctrl Pts',(127.032036789131,-76.0036363338475,-197.090005390471)) ;
#81586=CARTESIAN_POINT('Ctrl Pts',(127.032036789131,-75.8131363338475,-197.090005390471)) ;
#81587=CARTESIAN_POINT('Ctrl Pts',(127.481049604646,-75.8131363338475,-197.539018187062)) ;
#81588=CARTESIAN_POINT('',(127.260059362794,-75.8607613351713,-197.09000531248)) ;
#81589=CARTESIAN_POINT('Origin',(130.842036960973,-75.860761372679,-200.900005401736)) ;
#81590=CARTESIAN_POINT('Ctrl Pts',(128.000141404111,-75.8131363338475,-197.090005310182)) ;
#81591=CARTESIAN_POINT('Ctrl Pts',(127.875189846825,-75.8131363338475,-197.090005310182)) ;
#81592=CARTESIAN_POINT('Ctrl Pts',(127.74042967657,-75.8151139619557,-197.090005310065)) ;
#81593=CARTESIAN_POINT('Ctrl Pts',(127.489185117999,-75.8281618999272,-197.090005310065)) ;
#81594=CARTESIAN_POINT('Ctrl Pts',(127.362906128424,-75.8396272926172,-197.090005310182)) ;
#81595=CARTESIAN_POINT('Ctrl Pts',(127.260059363022,-75.8607613362829,-197.090005310182)) ;
#81596=CARTESIAN_POINT('Origin',(127.03203686942,-75.8131363338475,-197.090005310181)) ;
#81597=CARTESIAN_POINT('',(127.03203686942,-75.8607613336239,-197.31802783382)) ;
#81598=CARTESIAN_POINT('Origin',(134.65203686942,-75.8131363338475,-197.090005310183)) ;
#81599=CARTESIAN_POINT('',(127.260059374874,-75.8131363338475,-197.090005310181)) ;
#81600=CARTESIAN_POINT('Ctrl Pts',(127.032036789131,-76.0036363338475,-197.090005390471)) ;
#81601=CARTESIAN_POINT('Ctrl Pts',(127.032036789131,-75.8131363338475,-197.090005390471)) ;
#81602=CARTESIAN_POINT('Ctrl Pts',(127.481049604646,-75.8131363338475,-197.539018187062)) ;
#81603=CARTESIAN_POINT('Ctrl Pts',(123.222036869419,-76.0036363338475,-200.90000547076)) ;
#81604=CARTESIAN_POINT('Ctrl Pts',(123.222036869419,-75.8131363338475,-200.90000547076)) ;
#81605=CARTESIAN_POINT('Ctrl Pts',(124.120062481526,-75.8131363338475,-200.900005451836)) ;
#81606=CARTESIAN_POINT('Ctrl Pts',(127.032036949709,-76.0036363338475,-204.710005390471)) ;
#81607=CARTESIAN_POINT('Ctrl Pts',(127.032036949709,-75.8131363338475,-204.710005390471)) ;
#81608=CARTESIAN_POINT('Ctrl Pts',(127.4810497463,-75.8131363338475,-204.260992574956)) ;
#81609=CARTESIAN_POINT('Ctrl Pts',(130.842037029998,-76.0036363338476,-208.520005310182)) ;
#81610=CARTESIAN_POINT('Ctrl Pts',(130.842037029998,-75.8131363338476,-208.520005310182)) ;
#81611=CARTESIAN_POINT('Ctrl Pts',(130.842037011073,-75.8131363338476,-207.621979698075)) ;
#81612=CARTESIAN_POINT('Ctrl Pts',(134.652036949709,-76.0036363338476,-204.710005229893)) ;
#81613=CARTESIAN_POINT('Ctrl Pts',(134.652036949709,-75.8131363338476,-204.710005229893)) ;
#81614=CARTESIAN_POINT('Ctrl Pts',(134.203024134193,-75.8131363338476,-204.260992433302)) ;
#81615=CARTESIAN_POINT('Ctrl Pts',(138.46203686942,-76.0036363338475,-200.900005149604)) ;
#81616=CARTESIAN_POINT('Ctrl Pts',(138.46203686942,-75.8131363338475,-200.900005149604)) ;
#81617=CARTESIAN_POINT('Ctrl Pts',(137.564011257313,-75.8131363338475,-200.900005168529)) ;
#81618=CARTESIAN_POINT('Ctrl Pts',(134.652036789131,-76.0036363338475,-197.090005229893)) ;
#81619=CARTESIAN_POINT('Ctrl Pts',(134.652036789131,-75.8131363338475,-197.090005229893)) ;
#81620=CARTESIAN_POINT('Ctrl Pts',(134.203023992539,-75.8131363338475,-197.539018045409)) ;
#81621=CARTESIAN_POINT('Ctrl Pts',(130.842036708842,-76.0036363338475,-193.280005310182)) ;
#81622=CARTESIAN_POINT('Ctrl Pts',(130.842036708842,-75.8131363338475,-193.280005310182)) ;
#81623=CARTESIAN_POINT('Ctrl Pts',(130.842036727766,-75.8131363338475,-194.178030922289)) ;
#81624=CARTESIAN_POINT('Ctrl Pts',(127.032036789131,-76.0036363338475,-197.090005390471)) ;
#81625=CARTESIAN_POINT('Ctrl Pts',(127.032036789131,-75.8131363338475,-197.090005390471)) ;
#81626=CARTESIAN_POINT('Ctrl Pts',(127.481049604646,-75.8131363338475,-197.539018187062)) ;
#81627=CARTESIAN_POINT('',(134.65203686769,-75.8607613348134,-197.318027806949)) ;
#81628=CARTESIAN_POINT('',(134.424014355279,-75.8607613328816,-197.090005308453)) ;
#81629=CARTESIAN_POINT('Origin',(130.842036870408,-75.860761333849,-200.90000531117)) ;
#81630=CARTESIAN_POINT('Ctrl Pts',(134.424014355441,-75.8607613320954,-197.090005310183)) ;
#81631=CARTESIAN_POINT('Ctrl Pts',(134.32116716318,-75.8396272026364,-197.090005310183)) ;
#81632=CARTESIAN_POINT('Ctrl Pts',(134.194896423912,-75.8281624630208,-197.09000531008)) ;
#81633=CARTESIAN_POINT('Ctrl Pts',(133.943648193978,-75.8151140186795,-197.09000531008)) ;
#81634=CARTESIAN_POINT('Ctrl Pts',(133.80888568398,-75.8131363338475,-197.090005310183)) ;
#81635=CARTESIAN_POINT('Ctrl Pts',(133.68393233473,-75.8131363338475,-197.090005310183)) ;
#81636=CARTESIAN_POINT('Ctrl Pts',(134.65203686942,-75.8131363338475,-198.058109844874)) ;
#81637=CARTESIAN_POINT('Ctrl Pts',(134.65203686942,-75.8131363338475,-197.933158288262)) ;
#81638=CARTESIAN_POINT('Ctrl Pts',(134.652036869537,-75.8151139619343,-197.79839811889)) ;
#81639=CARTESIAN_POINT('Ctrl Pts',(134.652036869537,-75.8281618997332,-197.547153561353)) ;
#81640=CARTESIAN_POINT('Ctrl Pts',(134.65203686942,-75.8396272922763,-197.420874572373)) ;
#81641=CARTESIAN_POINT('Ctrl Pts',(134.65203686942,-75.8607613355994,-197.318027807111)) ;
#81642=CARTESIAN_POINT('Origin',(134.652036869419,-75.8131363338476,-204.710005310183)) ;
#81643=CARTESIAN_POINT('',(134.65203686942,-75.8131363338475,-197.318027815637)) ;
#81644=CARTESIAN_POINT('Origin',(134.65203686942,-75.8131363338475,-197.090005310183)) ;
#81645=CARTESIAN_POINT('',(134.424014351237,-75.860761333691,-197.090005310183)) ;
#81646=CARTESIAN_POINT('Origin',(130.84203686942,-75.8131363338475,-200.900005310182)) ;
#81647=CARTESIAN_POINT('Origin',(130.84203686942,-75.8131363338475,-200.900005310182)) ;
#81648=CARTESIAN_POINT('Origin',(130.84203686942,-75.8131363338475,-200.900005310182)) ;
#81649=CARTESIAN_POINT('Origin',(130.84203686942,-75.8131363338475,-200.900005310182)) ;
#86295=UNCERTAINTY_MEASURE_WITH_UNIT(LENGTH_MEASURE(0.01),#86331,
'DISTANCE_ACCURACY_VALUE',
'Maximum model space distance between geometric entities at asserted c
onnectivities') ;
#86304=UNCERTAINTY_MEASURE_WITH_UNIT(LENGTH_MEASURE(0.01),#86331,
'DISTANCE_ACCURACY_VALUE',
'Maximum model space distance between geometric entities at asserted c
onnectivities') ;
#86321=(
GEOMETRIC_REPRESENTATION_CONTEXT(3)
GLOBAL_UNCERTAINTY_ASSIGNED_CONTEXT((#86295))
GLOBAL_UNIT_ASSIGNED_CONTEXT((#86331,#86333,#86334))
REPRESENTATION_CONTEXT('','3D')
) ;
#86330=(
GEOMETRIC_REPRESENTATION_CONTEXT(3)
GLOBAL_UNCERTAINTY_ASSIGNED_CONTEXT((#86304))
GLOBAL_UNIT_ASSIGNED_CONTEXT((#86331,#86333,#86334))
REPRESENTATION_CONTEXT('','3D')
) ;
#86331=(
LENGTH_UNIT()
NAMED_UNIT(*)
SI_UNIT(.MILLI.,.METRE.)
) ;
#86333=(
NAMED_UNIT(*)
PLANE_ANGLE_UNIT()
SI_UNIT($,.RADIAN.)
) ;
#86334=(
NAMED_UNIT(*)
SI_UNIT($,.STERADIAN.)
SOLID_ANGLE_UNIT()
) ;
#86351=SHAPE_DEFINITION_REPRESENTATION(#86409,#86467) ;
#86409=PRODUCT_DEFINITION_SHAPE('',$,#86493) ;
#86467=SHAPE_REPRESENTATION('',(#36144),#86321) ;
#86476=PRODUCT_DEFINITION_CONTEXT('part definition',#86553,'design') ;
#86493=PRODUCT_DEFINITION('Flat_Washer_Large','Flat_Washer_Large',#86518,
#86476) ;
#86518=PRODUCT_DEFINITION_FORMATION('',$,#86571) ;
#86553=APPLICATION_CONTEXT(
'Core Data for Automotive Mechanical Design Process') ;
#86554=PRODUCT_CONTEXT('part definition',#86553,'mechanical') ;
#86571=PRODUCT('Flat_Washer_Large','Flat_Washer_Large',$,(#86554)) ;
#86582=PRESENTATION_STYLE_ASSIGNMENT((#86587)) ;
#86587=SURFACE_STYLE_USAGE(.BOTH.,#86592) ;
#86592=SURFACE_SIDE_STYLE('',(#86597)) ;
#86597=SURFACE_STYLE_FILL_AREA(#86602) ;
#86602=FILL_AREA_STYLE('Opaque(203,203,203)',(#86607)) ;
#86607=FILL_AREA_STYLE_COLOUR('Opaque(203,203,203)',#86612) ;
#86612=COLOUR_RGB('Opaque(203,203,203)', 0.66274510, 0.83137255, 0.94901961) ;
ENDSEC;
END-ISO-10303-21;
